ISO-10303-21;
HEADER;
FILE_DESCRIPTION (('STEP AP214'),
    '1' );
FILE_NAME ('spur gear_iso_ISO - Spur gear 2M 20T 20PA 8FW ---S20A75H50L8.0S1.step',
    '2026-09-28T15:49:00',
    ( '' ),
    ( '' ),
    'SwSTEP 2.0',
    'SolidWorks 2026',
    '' );
FILE_SCHEMA (( 'AUTOMOTIVE_DESIGN' ));
ENDSEC;

DATA;
#2=CARTESIAN_POINT ( 'NONE',  ( 8.000000000000000000, 0.000000000000000000, 0.000000000000000000 ) ) ;
#10=ORIENTED_EDGE ( 'NONE', *, *, #14256, .F. ) ;
#37=ORIENTED_EDGE ( 'NONE', *, *, #7435, .F. ) ;
#46=AXIS2_PLACEMENT_3D ( 'NONE', #19606, #14217, #25394 ) ;
#66=EDGE_CURVE ( 'NONE', #4339, #26513, #34817, .T. ) ;
#73=CYLINDRICAL_SURFACE ( 'NONE', #12884, 22.00000000000000000 ) ;
#92=DIRECTION ( 'NONE',  ( 0.000000000000000000, 0.000000000000000000, 1.000000000000000000 ) ) ;
#99=AXIS2_PLACEMENT_3D ( 'NONE', #28579, #20265, #1214 ) ;
#122=FILL_AREA_STYLE_COLOUR ( '', #22409 ) ;
#132=DIRECTION ( 'NONE',  ( -1.000000000000000000, 0.000000000000000000, 0.000000000000000000 ) ) ;
#147=CARTESIAN_POINT ( 'NONE',  ( 0.000000000000000000, -3.968388925834656966, -21.63912866391144618 ) ) ;
#157=DIRECTION ( 'NONE',  ( 0.000000000000000000, 0.000000000000000000, 1.000000000000000000 ) ) ;
#159=DIRECTION ( 'NONE',  ( 0.000000000000000000, -0.9510565162951564178, 0.3090169943749385140 ) ) ;
#180=VERTEX_POINT ( 'NONE', #14854 ) ;
#197=EDGE_CURVE ( 'NONE', #14850, #9043, #11214, .T. ) ;
#220=DIRECTION ( 'NONE',  ( -0.000000000000000000, 1.000000000000000000, 0.000000000000000000 ) ) ;
#227=ORIENTED_EDGE ( 'NONE', *, *, #23757, .T. ) ;
#232=EDGE_CURVE ( 'NONE', #25838, #30814, #21546, .T. ) ;
#245=DIRECTION ( 'NONE',  ( 0.000000000000000000, 0.000000000000000000, 1.000000000000000000 ) ) ;
#249=LINE ( 'NONE', #5836, #8196 ) ;
#251=VERTEX_POINT ( 'NONE', #7468 ) ;
#258=DIRECTION ( 'NONE',  ( -1.000000000000000000, 0.000000000000000000, 0.000000000000000000 ) ) ;
#272=VERTEX_POINT ( 'NONE', #18447 ) ;
#277=DIRECTION ( 'NONE',  ( -1.000000000000000000, 0.000000000000000000, 0.000000000000000000 ) ) ;
#280=CARTESIAN_POINT ( 'NONE',  ( 0.000000000000000000, 0.000000000000000000, 0.000000000000000000 ) ) ;
#282=EDGE_CURVE ( 'NONE', #12434, #12602, #7107, .T. ) ;
#312=EDGE_CURVE ( 'NONE', #5963, #29170, #3617, .T. ) ;
#315=AXIS2_PLACEMENT_3D ( 'NONE', #2102, #4970, #28914 ) ;
#319=CARTESIAN_POINT ( 'NONE',  ( 8.000000000000000000, 0.000000000000000000, 0.000000000000000000 ) ) ;
#340=VECTOR ( 'NONE', #10135, 1000.000000000000000 ) ;
#356=ORIENTED_EDGE ( 'NONE', *, *, #3793, .T. ) ;
#364=VECTOR ( 'NONE', #24765, 1000.000000000000000 ) ;
#367=CARTESIAN_POINT ( 'NONE',  ( 8.000000000000000000, 21.80633394113452539, 2.912696353505896951 ) ) ;
#402=DIRECTION ( 'NONE',  ( 0.000000000000000000, -0.3090169943749350723, -0.9510565162951575280 ) ) ;
#426=AXIS2_PLACEMENT_3D ( 'NONE', #32589, #7921, #10816 ) ;
#430=CYLINDRICAL_SURFACE ( 'NONE', #31948, 8.000000000000001776 ) ;
#450=EDGE_CURVE ( 'NONE', #2681, #869, #20260, .T. ) ;
#472=DIRECTION ( 'NONE',  ( 0.000000000000000000, 0.000000000000000000, -1.000000000000000000 ) ) ;
#474=ADVANCED_FACE ( 'NONE', ( #13068 ), #24053, .T. ) ;
#483=DIRECTION ( 'NONE',  ( -1.000000000000000000, 0.000000000000000000, 0.000000000000000000 ) ) ;
#495=CIRCLE ( 'NONE', #14285, 8.000000000000007105 ) ;
#501=ORIENTED_EDGE ( 'NONE', *, *, #19569, .T. ) ;
#511=ADVANCED_FACE ( 'NONE', ( #8700 ), #3145, .T. ) ;
#519=VERTEX_POINT ( 'NONE', #9064 ) ;
#521=ORIENTED_EDGE ( 'NONE', *, *, #7435, .T. ) ;
#538=CARTESIAN_POINT ( 'NONE',  ( 3.999999999999996447, -2.912696353505970226, 21.80633394113446499 ) ) ;
#554=DIRECTION ( 'NONE',  ( 0.000000000000000000, -0.8090169943749405679, -0.5877852522924827960 ) ) ;
#573=ORIENTED_EDGE ( 'NONE', *, *, #27913, .F. ) ;
#581=ORIENTED_EDGE ( 'NONE', *, *, #5080, .F. ) ;
#594=CYLINDRICAL_SURFACE ( 'NONE', #29679, 8.000000000000001776 ) ;
#601=DIRECTION ( 'NONE',  ( 1.000000000000000000, -0.000000000000000000, -0.000000000000000000 ) ) ;
#609=CARTESIAN_POINT ( 'NONE',  ( 8.000000000000000000, -11.06713717293248855, 13.55483219355725844 ) ) ;
#614=CARTESIAN_POINT ( 'NONE',  ( 8.000000000000000000, -18.48663108841356717, -3.384281271888017084 ) ) ;
#643=CARTESIAN_POINT ( 'NONE',  ( 8.000000000000000000, 14.71414642875970635, -9.471478019454975694 ) ) ;
#664=EDGE_CURVE ( 'NONE', #29327, #20524, #13938, .T. ) ;
#671=DIRECTION ( 'NONE',  ( -1.000000000000000000, 0.000000000000000000, 0.000000000000000000 ) ) ;
#724=EDGE_CURVE ( 'NONE', #25690, #31502, #33542, .T. ) ;
#739=LINE ( 'NONE', #3114, #13317 ) ;
#760=ORIENTED_EDGE ( 'NONE', *, *, #7391, .T. ) ;
#768=CARTESIAN_POINT ( 'NONE',  ( 0.000000000000000000, 15.17386234660407140, -15.92965478239605304 ) ) ;
#772=CARTESIAN_POINT ( 'NONE',  ( 0.000000000000000000, -14.71414642875963708, 9.471478019455089381 ) ) ;
#785=DIRECTION ( 'NONE',  ( 1.000000000000000000, -0.000000000000000000, 0.000000000000000000 ) ) ;
#797=ORIENTED_EDGE ( 'NONE', *, *, #33317, .T. ) ;
#805=DIRECTION ( 'NONE',  ( 0.000000000000000000, 0.000000000000000000, 1.000000000000000000 ) ) ;
#817=CIRCLE ( 'NONE', #23843, 8.000000000000008882 ) ;
#831=EDGE_CURVE ( 'NONE', #31433, #8092, #15696, .T. ) ;
#843=CARTESIAN_POINT ( 'NONE',  ( 0.000000000000000000, 21.80633394113450052, -2.912696353505896063 ) ) ;
#847=VECTOR ( 'NONE', #27852, 1000.000000000000000 ) ;
#859=AXIS2_PLACEMENT_3D ( 'NONE', #7769, #4918, #5101 ) ;
#869=VERTEX_POINT ( 'NONE', #13202 ) ;
#920=CYLINDRICAL_SURFACE ( 'NONE', #19895, 22.00000000000000000 ) ;
#940=ORIENTED_EDGE ( 'NONE', *, *, #3703, .F. ) ;
#954=EDGE_CURVE ( 'NONE', #1113, #17966, #12270, .T. ) ;
#975=ADVANCED_FACE ( 'NONE', ( #5278 ), #19470, .T. ) ;
#996=CYLINDRICAL_SURFACE ( 'NONE', #1858, 8.000000000000001776 ) ;
#1017=AXIS2_PLACEMENT_3D ( 'NONE', #35598, #30184, #13621 ) ;
#1018=CARTESIAN_POINT ( 'NONE',  ( 8.000000000000000000, 0.000000000000000000, 0.000000000000000000 ) ) ;
#1020=ORIENTED_EDGE ( 'NONE', *, *, #16886, .T. ) ;
#1025=ORIENTED_EDGE ( 'NONE', *, *, #23489, .F. ) ;
#1074=VERTEX_POINT ( 'NONE', #8659 ) ;
#1082=ORIENTED_EDGE ( 'NONE', *, *, #21395, .T. ) ;
#1113=VERTEX_POINT ( 'NONE', #30633 ) ;
#1120=AXIS2_PLACEMENT_3D ( 'NONE', #13278, #13615, #19015 ) ;
#1137=CARTESIAN_POINT ( 'NONE',  ( 8.000000000000000000, -19.35373470438990395, 10.46102064772334295 ) ) ;
#1163=ORIENTED_EDGE ( 'NONE', *, *, #4540, .F. ) ;
#1164=ADVANCED_FACE ( 'NONE', ( #8300 ), #19281, .T. ) ;
#1173=AXIS2_PLACEMENT_3D ( 'NONE', #22821, #28072, #3949 ) ;
#1177=AXIS2_PLACEMENT_3D ( 'NONE', #16266, #8007, #18991 ) ;
#1184=DIRECTION ( 'NONE',  ( -1.000000000000000000, 0.000000000000000000, 0.000000000000000000 ) ) ;
#1202=ORIENTED_EDGE ( 'NONE', *, *, #14635, .F. ) ;
#1207=EDGE_CURVE ( 'NONE', #32151, #22471, #34416, .T. ) ;
#1214=DIRECTION ( 'NONE',  ( 0.000000000000000000, 0.000000000000000000, 1.000000000000000000 ) ) ;
#1218=DIRECTION ( 'NONE',  ( 0.000000000000000000, -6.938893903907226800E-15, 1.000000000000000000 ) ) ;
#1272=VECTOR ( 'NONE', #31102, 1000.000000000000000 ) ;
#1287=ORIENTED_EDGE ( 'NONE', *, *, #1502, .T. ) ;
#1296=DIRECTION ( 'NONE',  ( -1.000000000000000000, 0.000000000000000000, 0.000000000000000000 ) ) ;
#1310=CIRCLE ( 'NONE', #10514, 8.000000000000007105 ) ;
#1315=CARTESIAN_POINT ( 'NONE',  ( 4.000000000000003553, -19.35373470438975119, -10.46102064772362183 ) ) ;
#1318=DIRECTION ( 'NONE',  ( 0.000000000000000000, 0.000000000000000000, -1.000000000000000000 ) ) ;
#1346=APPLICATION_CONTEXT ( 'automotive_design' ) ;
#1352=CARTESIAN_POINT ( 'NONE',  ( -10.00000000000000178, 0.000000000000000000, 0.000000000000000000 ) ) ;
#1361=CYLINDRICAL_SURFACE ( 'NONE', #19930, 22.00000000000000000 ) ;
#1362=AXIS2_PLACEMENT_3D ( 'NONE', #33621, #17230, #14707 ) ;
#1368=ORIENTED_EDGE ( 'NONE', *, *, #5758, .F. ) ;
#1372=LINE ( 'NONE', #17554, #8380 ) ;
#1409=EDGE_CURVE ( 'NONE', #869, #29036, #15654, .T. ) ;
#1429=CYLINDRICAL_SURFACE ( 'NONE', #5829, 8.000000000000001776 ) ;
#1437=CIRCLE ( 'NONE', #35374, 8.000000000000000000 ) ;
#1476=CIRCLE ( 'NONE', #12397, 8.000000000000007105 ) ;
#1488=CIRCLE ( 'NONE', #20450, 8.000000000000001776 ) ;
#1490=CARTESIAN_POINT ( 'NONE',  ( 8.000000000000000000, 17.47118961583601759, 0.9861715913088272556 ) ) ;
#1502=EDGE_CURVE ( 'NONE', #1815, #16380, #2008, .T. ) ;
#1507=ORIENTED_EDGE ( 'NONE', *, *, #19965, .F. ) ;
#1531=ADVANCED_FACE ( 'NONE', ( #24672 ), #24146, .T. ) ;
#1532=CIRCLE ( 'NONE', #14752, 8.000000000000000000 ) ;
#1533=DIRECTION ( 'NONE',  ( 0.000000000000000000, -0.3090169943749350723, -0.9510565162951576390 ) ) ;
#1541=VECTOR ( 'NONE', #2445, 1000.000000000000000 ) ;
#1547=EDGE_CURVE ( 'NONE', #8636, #2129, #21952, .T. ) ;
#1554=ORIENTED_EDGE ( 'NONE', *, *, #29760, .F. ) ;
#1557=DIRECTION ( 'NONE',  ( 1.000000000000000000, -0.000000000000000000, 0.000000000000000000 ) ) ;
#1567=VECTOR ( 'NONE', #22266, 1000.000000000000000 ) ;
#1569=ADVANCED_FACE ( 'NONE', ( #13342 ), #24323, .T. ) ;
#1602=ORIENTED_EDGE ( 'NONE', *, *, #31055, .T. ) ;
#1616=VERTEX_POINT ( 'NONE', #9158 ) ;
#1617=VERTEX_POINT ( 'NONE', #25384 ) ;
#1622=LINE ( 'NONE', #12601, #30461 ) ;
#1659=EDGE_CURVE ( 'NONE', #8935, #35010, #12896, .T. ) ;
#1674=LINE ( 'NONE', #15504, #30118 ) ;
#1687=AXIS2_PLACEMENT_3D ( 'NONE', #17179, #11265, #28357 ) ;
#1689=DIRECTION ( 'NONE',  ( -1.000000000000000000, 0.000000000000000000, 0.000000000000000000 ) ) ;
#1690=CARTESIAN_POINT ( 'NONE',  ( 8.000000000000000000, 16.94522934049224361, -8.128228055638670568 ) ) ;
#1701=ORIENTED_EDGE ( 'NONE', *, *, #25097, .F. ) ;
#1707=DIRECTION ( 'NONE',  ( 0.000000000000000000, 0.5877852522924738032, -0.8090169943749468962 ) ) ;
#1729=DIRECTION ( 'NONE',  ( 0.000000000000000000, 0.000000000000000000, -1.000000000000000000 ) ) ;
#1734=CARTESIAN_POINT ( 'NONE',  ( -10.00000000000000178, 0.000000000000000000, 0.000000000000000000 ) ) ;
#1735=EDGE_LOOP ( 'NONE', ( #29650, #4168, #5761, #15446 ) ) ;
#1751=CARTESIAN_POINT ( 'NONE',  ( 8.000000000000000000, 3.384281271887823461, 18.48663108841358138 ) ) ;
#1755=DIRECTION ( 'NONE',  ( 0.000000000000000000, 0.3090169943749412895, 0.9510565162951555296 ) ) ;
#1770=DIRECTION ( 'NONE',  ( -1.000000000000000000, 0.000000000000000000, 0.000000000000000000 ) ) ;
#1783=CYLINDRICAL_SURFACE ( 'NONE', #24407, 17.49900000000000233 ) ;
#1789=EDGE_CURVE ( 'NONE', #14155, #2828, #19197, .T. ) ;
#1815=VERTEX_POINT ( 'NONE', #7167 ) ;
#1820=EDGE_LOOP ( 'NONE', ( #13899, #19294, #31503, #24102 ) ) ;
#1838=CARTESIAN_POINT ( 'NONE',  ( 8.000000000000000000, 2.494040418455619523, -18.62763138773847871 ) ) ;
#1847=VERTEX_POINT ( 'NONE', #9518 ) ;
#1856=AXIS2_PLACEMENT_3D ( 'NONE', #29919, #7940, #2564 ) ;
#1858=AXIS2_PLACEMENT_3D ( 'NONE', #20395, #33939, #9270 ) ;
#1863=ORIENTED_EDGE ( 'NONE', *, *, #11605, .F. ) ;
#1864=LINE ( 'NONE', #23266, #22863 ) ;
#1881=ORIENTED_EDGE ( 'NONE', *, *, #30112, .F. ) ;
#1883=ADVANCED_FACE ( 'NONE', ( #26448 ), #1783, .T. ) ;
#1908=DIRECTION ( 'NONE',  ( 1.000000000000000000, -0.000000000000000000, 0.000000000000000000 ) ) ;
#1917=CARTESIAN_POINT ( 'NONE',  ( 8.000000000000000000, 21.80633394113450052, -2.912696353505896951 ) ) ;
#1961=LINE ( 'NONE', #29150, #27512 ) ;
#1988=CYLINDRICAL_SURFACE ( 'NONE', #23361, 8.000000000000001776 ) ;
#2004=EDGE_LOOP ( 'NONE', ( #5462, #27280, #12409, #29157 ) ) ;
#2008=LINE ( 'NONE', #10634, #17443 ) ;
#2013=CIRCLE ( 'NONE', #14696, 8.000000000000007105 ) ;
#2018=CARTESIAN_POINT ( 'NONE',  ( 8.000000000000000000, 15.17386234660406785, -15.92965478239604948 ) ) ;
#2020=DIRECTION ( 'NONE',  ( -1.000000000000000000, 0.000000000000000000, 0.000000000000000000 ) ) ;
#2023=EDGE_LOOP ( 'NONE', ( #27120, #25925, #32769, #521 ) ) ;
#2034=CARTESIAN_POINT ( 'NONE',  ( 4.000000000000003553, -15.92965478239607968, -15.17386234660401101 ) ) ;
#2072=EDGE_CURVE ( 'NONE', #25710, #20884, #22267, .T. ) ;
#2073=DIRECTION ( 'NONE',  ( -1.000000000000000000, 0.000000000000000000, 0.000000000000000000 ) ) ;
#2077=EDGE_CURVE ( 'NONE', #7954, #25710, #12338, .T. ) ;
#2097=CARTESIAN_POINT ( 'NONE',  ( 3.999999999999996447, -21.80633394113452539, 2.912696353505744185 ) ) ;
#2101=VECTOR ( 'NONE', #30695, 1000.000000000000000 ) ;
#2102=CARTESIAN_POINT ( 'NONE',  ( 8.000000000000000000, 0.000000000000000000, 0.000000000000000000 ) ) ;
#2104=ORIENTED_EDGE ( 'NONE', *, *, #28162, .F. ) ;
#2108=CARTESIAN_POINT ( 'NONE',  ( 0.000000000000000000, 0.000000000000000000, 0.000000000000000000 ) ) ;
#2111=VERTEX_POINT ( 'NONE', #22091 ) ;
#2115=VERTEX_POINT ( 'NONE', #19389 ) ;
#2116=CARTESIAN_POINT ( 'NONE',  ( 4.000000000000003553, 15.17386234660407140, -15.92965478239605304 ) ) ;
#2126=CARTESIAN_POINT ( 'NONE',  ( 0.000000000000000000, 0.000000000000000000, 0.000000000000000000 ) ) ;
#2129=VERTEX_POINT ( 'NONE', #21915 ) ;
#2174=DIRECTION ( 'NONE',  ( -1.000000000000000000, 0.000000000000000000, 0.000000000000000000 ) ) ;
#2213=AXIS2_PLACEMENT_3D ( 'NONE', #31489, #26629, #31832 ) ;
#2214=CARTESIAN_POINT ( 'NONE',  ( 4.000000000000003553, 15.92965478239641008, -15.17386234660366284 ) ) ;
#2226=ADVANCED_FACE ( 'NONE', ( #3202 ), #13820, .T. ) ;
#2249=ORIENTED_EDGE ( 'NONE', *, *, #7391, .F. ) ;
#2250=ORIENTED_EDGE ( 'NONE', *, *, #33891, .T. ) ;
#2261=EDGE_CURVE ( 'NONE', #18178, #17571, #6573, .T. ) ;
#2283=DIRECTION ( 'NONE',  ( 0.000000000000000000, 0.000000000000000000, 1.000000000000000000 ) ) ;
#2289=DIRECTION ( 'NONE',  ( 0.000000000000000000, -6.983129352544636959E-15, 1.000000000000000000 ) ) ;
#2297=ORIENTED_EDGE ( 'NONE', *, *, #11976, .F. ) ;
#2317=DIRECTION ( 'NONE',  ( -1.000000000000000000, 0.000000000000000000, 0.000000000000000000 ) ) ;
#2320=DIRECTION ( 'NONE',  ( 0.000000000000000000, 0.8090169943749448977, 0.5877852522924766898 ) ) ;
#2323=AXIS2_PLACEMENT_3D ( 'NONE', #12509, #34482, #9801 ) ;
#2348=ORIENTED_EDGE ( 'NONE', *, *, #9015, .F. ) ;
#2360=ORIENTED_EDGE ( 'NONE', *, *, #664, .F. ) ;
#2365=ORIENTED_EDGE ( 'NONE', *, *, #14298, .T. ) ;
#2371=LINE ( 'NONE', #24845, #7352 ) ;
#2378=ORIENTED_EDGE ( 'NONE', *, *, #7347, .T. ) ;
#2382=CIRCLE ( 'NONE', #22462, 22.00000000000000000 ) ;
#2391=CARTESIAN_POINT ( 'NONE',  ( 8.000000000000000000, 11.06713717293261467, -13.55483219355716606 ) ) ;
#2434=ADVANCED_FACE ( 'NONE', ( #24236 ), #21335, .T. ) ;
#2435=CARTESIAN_POINT ( 'NONE',  ( 8.000000000000000000, 12.96676809804150565, 13.60411018104323411 ) ) ;
#2445=DIRECTION ( 'NONE',  ( -1.000000000000000000, 0.000000000000000000, 0.000000000000000000 ) ) ;
#2453=DIRECTION ( 'NONE',  ( 0.000000000000000000, 0.000000000000000000, 1.000000000000000000 ) ) ;
#2457=DIRECTION ( 'NONE',  ( -1.000000000000000000, 0.000000000000000000, 0.000000000000000000 ) ) ;
#2464=EDGE_CURVE ( 'NONE', #23346, #16643, #4977, .T. ) ;
#2465=CIRCLE ( 'NONE', #13931, 4.000000000000000000 ) ;
#2468=CARTESIAN_POINT ( 'NONE',  ( 8.000000000000000000, -18.62763138773852134, 2.494040418455287345 ) ) ;
#2472=DIRECTION ( 'NONE',  ( 0.000000000000000000, 1.000000000000000000, 3.491564676272318479E-15 ) ) ;
#2475=CIRCLE ( 'NONE', #30621, 22.00000000000000000 ) ;
#2476=CARTESIAN_POINT ( 'NONE',  ( 3.999999999999996447, 21.63912866391145684, -3.968388925834583247 ) ) ;
#2532=CARTESIAN_POINT ( 'NONE',  ( 8.000000000000000000, -21.63912866391137513, -3.968388925835035330 ) ) ;
#2550=ORIENTED_EDGE ( 'NONE', *, *, #33478, .T. ) ;
#2564=DIRECTION ( 'NONE',  ( 0.000000000000000000, -0.5877852522924620349, -0.8090169943749554449 ) ) ;
#2604=AXIS2_PLACEMENT_3D ( 'NONE', #21534, #4497, #31827 ) ;
#2624=DIRECTION ( 'NONE',  ( -1.000000000000000000, 0.000000000000000000, 0.000000000000000000 ) ) ;
#2633=ORIENTED_EDGE ( 'NONE', *, *, #13327, .T. ) ;
#2637=CYLINDRICAL_SURFACE ( 'NONE', #11671, 8.000000000000001776 ) ;
#2649=ADVANCED_FACE ( 'NONE', ( #30519 ), #2637, .T. ) ;
#2669=DIRECTION ( 'NONE',  ( 0.000000000000000000, 0.000000000000000000, 1.000000000000000000 ) ) ;
#2672=CARTESIAN_POINT ( 'NONE',  ( 50.00005079999999680, 4.898587196589412829E-16, -4.000000000000000000 ) ) ;
#2681=VERTEX_POINT ( 'NONE', #10910 ) ;
#2692=ORIENTED_EDGE ( 'NONE', *, *, #312, .T. ) ;
#2711=EDGE_CURVE ( 'NONE', #26583, #1113, #24942, .T. ) ;
#2718=EDGE_LOOP ( 'NONE', ( #11417, #19553, #16467, #11464 ) ) ;
#2734=AXIS2_PLACEMENT_3D ( 'NONE', #30386, #483, #11461 ) ;
#2740=VECTOR ( 'NONE', #9136, 1000.000000000000000 ) ;
#2749=CIRCLE ( 'NONE', #19392, 17.49900000000000233 ) ;
#2778=ORIENTED_EDGE ( 'NONE', *, *, #4611, .T. ) ;
#2785=( NAMED_UNIT ( * ) SI_UNIT ( $, .STERADIAN. ) SOLID_ANGLE_UNIT ( ) );
#2810=CARTESIAN_POINT ( 'NONE',  ( 8.000000000000000000, 3.384281271888069487, -18.48663108841355296 ) ) ;
#2818=CYLINDRICAL_SURFACE ( 'NONE', #11245, 17.49900000000000233 ) ;
#2826=ORIENTED_EDGE ( 'NONE', *, *, #5262, .T. ) ;
#2828=VERTEX_POINT ( 'NONE', #26002 ) ;
#2829=ORIENTED_EDGE ( 'NONE', *, *, #29760, .T. ) ;
#2834=ORIENTED_EDGE ( 'NONE', *, *, #18767, .T. ) ;
#2845=CARTESIAN_POINT ( 'NONE',  ( 4.000000000000003553, -9.508666619816789733, 19.83898331853681896 ) ) ;
#2862=ORIENTED_EDGE ( 'NONE', *, *, #6391, .F. ) ;
#2872=DIRECTION ( 'NONE',  ( 0.000000000000000000, 0.000000000000000000, -1.000000000000000000 ) ) ;
#2881=DIRECTION ( 'NONE',  ( -1.000000000000000000, 0.000000000000000000, 0.000000000000000000 ) ) ;
#2912=ORIENTED_EDGE ( 'NONE', *, *, #11957, .F. ) ;
#2930=ADVANCED_FACE ( 'NONE', ( #10143 ), #18419, .T. ) ;
#2936=ORIENTED_EDGE ( 'NONE', *, *, #24914, .F. ) ;
#2938=LINE ( 'NONE', #8303, #31408 ) ;
#2948=EDGE_LOOP ( 'NONE', ( #12283, #16111, #1287, #33253 ) ) ;
#2966=COLOUR_RGB ( '', 0.31764706, 0.68627451, 0.89019608) ;
#2967=AXIS2_PLACEMENT_3D ( 'NONE', #12771, #21216, #15618 ) ;
#2986=EDGE_CURVE ( 'NONE', #23201, #9658, #1674, .T. ) ;
#2995=ORIENTED_EDGE ( 'NONE', *, *, #14778, .F. ) ;
#3020=CYLINDRICAL_SURFACE ( 'NONE', #14368, 8.000000000000001776 ) ;
#3026=ORIENTED_EDGE ( 'NONE', *, *, #15289, .F. ) ;
#3030=DIRECTION ( 'NONE',  ( -1.000000000000000000, 0.000000000000000000, 0.000000000000000000 ) ) ;
#3031=ORIENTED_EDGE ( 'NONE', *, *, #3176, .T. ) ;
#3035=AXIS2_PLACEMENT_3D ( 'NONE', #15538, #32300, #7620 ) ;
#3068=ORIENTED_EDGE ( 'NONE', *, *, #6816, .T. ) ;
#3080=CARTESIAN_POINT ( 'NONE',  ( 0.000000000000000000, 17.47118961583601404, -0.9861715913088251462 ) ) ;
#3081=ADVANCED_FACE ( 'NONE', ( #12656 ), #34449, .T. ) ;
#3084=VERTEX_POINT ( 'NONE', #1137 ) ;
#3103=VERTEX_POINT ( 'NONE', #29030 ) ;
#3109=DIRECTION ( 'NONE',  ( 0.000000000000000000, 0.5877852522924739143, -0.8090169943749468962 ) ) ;
#3114=CARTESIAN_POINT ( 'NONE',  ( 4.000000000000003553, -15.92965478239629817, 15.17386234660378008 ) ) ;
#3126=ORIENTED_EDGE ( 'NONE', *, *, #33275, .F. ) ;
#3130=CARTESIAN_POINT ( 'NONE',  ( 8.000000000000000000, -18.48663108841356717, 4.615718728111985136 ) ) ;
#3140=DIRECTION ( 'NONE',  ( -1.000000000000000000, 0.000000000000000000, 0.000000000000000000 ) ) ;
#3145=CYLINDRICAL_SURFACE ( 'NONE', #12822, 22.00000000000000000 ) ;
#3164=EDGE_CURVE ( 'NONE', #23592, #17129, #34256, .T. ) ;
#3173=AXIS2_PLACEMENT_3D ( 'NONE', #26345, #13198, #35339 ) ;
#3176=EDGE_CURVE ( 'NONE', #5736, #19206, #13010, .T. ) ;
#3177=DIRECTION ( 'NONE',  ( 0.000000000000000000, 0.000000000000000000, 1.000000000000000000 ) ) ;
#3190=AXIS2_PLACEMENT_3D ( 'NONE', #35359, #29783, #26911 ) ;
#3202=FACE_OUTER_BOUND ( 'NONE', #11847, .T. ) ;
#3209=DIRECTION ( 'NONE',  ( -1.000000000000000000, 0.000000000000000000, 0.000000000000000000 ) ) ;
#3231=CARTESIAN_POINT ( 'NONE',  ( 0.000000000000000000, 0.000000000000000000, 0.000000000000000000 ) ) ;
#3241=ORIENTED_EDGE ( 'NONE', *, *, #35015, .T. ) ;
#3248=DIRECTION ( 'NONE',  ( -1.000000000000000000, 0.000000000000000000, 0.000000000000000000 ) ) ;
#3261=ORIENTED_EDGE ( 'NONE', *, *, #16911, .T. ) ;
#3263=CIRCLE ( 'NONE', #7842, 4.000000000000000000 ) ;
#3264=CIRCLE ( 'NONE', #15311, 17.49900000000001654 ) ;
#3265=CIRCLE ( 'NONE', #17034, 22.00000000000000000 ) ;
#3271=DIRECTION ( 'NONE',  ( -1.000000000000000000, 0.000000000000000000, 0.000000000000000000 ) ) ;
#3274=DIRECTION ( 'NONE',  ( -1.000000000000000000, 0.000000000000000000, 0.000000000000000000 ) ) ;
#3277=ORIENTED_EDGE ( 'NONE', *, *, #8445, .T. ) ;
#3279=CARTESIAN_POINT ( 'NONE',  ( -10.00000000000000178, 0.000000000000000000, 0.000000000000000000 ) ) ;
#3285=VECTOR ( 'NONE', #13983, 1000.000000000000000 ) ;
#3312=VECTOR ( 'NONE', #3271, 1000.000000000000000 ) ;
#3322=DIRECTION ( 'NONE',  ( -1.000000000000000000, 0.000000000000000000, 0.000000000000000000 ) ) ;
#3335=LINE ( 'NONE', #609, #340 ) ;
#3342=DIRECTION ( 'NONE',  ( -1.000000000000000000, 0.000000000000000000, 0.000000000000000000 ) ) ;
#3359=DIRECTION ( 'NONE',  ( 0.000000000000000000, 0.000000000000000000, 1.000000000000000000 ) ) ;
#3364=LINE ( 'NONE', #22586, #35253 ) ;
#3365=LINE ( 'NONE', #5525, #12294 ) ;
#3386=DIRECTION ( 'NONE',  ( -1.000000000000000000, 0.000000000000000000, 0.000000000000000000 ) ) ;
#3387=CARTESIAN_POINT ( 'NONE',  ( 8.000000000000000000, 18.62763138773855687, 2.494040418455418351 ) ) ;
#3411=DIRECTION ( 'NONE',  ( -1.000000000000000000, 0.000000000000000000, 0.000000000000000000 ) ) ;
#3413=CARTESIAN_POINT ( 'NONE',  ( 8.000000000000000000, -2.912696353505969338, 21.80633394113446499 ) ) ;
#3414=DIRECTION ( 'NONE',  ( -1.000000000000000000, 0.000000000000000000, 0.000000000000000000 ) ) ;
#3432=DIRECTION ( 'NONE',  ( -1.000000000000000000, 0.000000000000000000, 0.000000000000000000 ) ) ;
#3455=EDGE_CURVE ( 'NONE', #34251, #34512, #5894, .T. ) ;
#3456=ORIENTED_EDGE ( 'NONE', *, *, #20900, .T. ) ;
#3459=DIRECTION ( 'NONE',  ( 0.000000000000000000, 0.000000000000000000, 1.000000000000000000 ) ) ;
#3460=VERTEX_POINT ( 'NONE', #367 ) ;
#3480=VERTEX_POINT ( 'NONE', #24696 ) ;
#3484=ORIENTED_EDGE ( 'NONE', *, *, #10018, .F. ) ;
#3488=DIRECTION ( 'NONE',  ( -1.000000000000000000, 0.000000000000000000, 0.000000000000000000 ) ) ;
#3499=CARTESIAN_POINT ( 'NONE',  ( 0.000000000000000000, -8.931325931664478190, -16.53603053422218494 ) ) ;
#3503=DIRECTION ( 'NONE',  ( -1.000000000000000000, 0.000000000000000000, 0.000000000000000000 ) ) ;
#3514=VECTOR ( 'NONE', #32219, 1000.000000000000000 ) ;
#3519=ORIENTED_EDGE ( 'NONE', *, *, #10818, .F. ) ;
#3564=ORIENTED_EDGE ( 'NONE', *, *, #19723, .F. ) ;
#3617=CIRCLE ( 'NONE', #33517, 8.000000000000008882 ) ;
#3636=AXIS2_PLACEMENT_3D ( 'NONE', #10128, #21094, #7428 ) ;
#3648=AXIS2_PLACEMENT_3D ( 'NONE', #11320, #16700, #8432 ) ;
#3656=ORIENTED_EDGE ( 'NONE', *, *, #5080, .T. ) ;
#3703=EDGE_CURVE ( 'NONE', #23592, #26583, #31800, .T. ) ;
#3707=LINE ( 'NONE', #12156, #33569 ) ;
#3708=ORIENTED_EDGE ( 'NONE', *, *, #20910, .T. ) ;
#3726=CARTESIAN_POINT ( 'NONE',  ( 8.000000000000000000, 14.71414642875970635, -9.471478019454975694 ) ) ;
#3736=CARTESIAN_POINT ( 'NONE',  ( 8.000000000000000000, 18.48663108841359559, 4.615718728112120139 ) ) ;
#3741=CARTESIAN_POINT ( 'NONE',  ( 8.000000000000000000, -6.336799421339930127, 16.31134495048480915 ) ) ;
#3748=DIRECTION ( 'NONE',  ( 0.000000000000000000, -0.8090169943749405679, -0.5877852522924826850 ) ) ;
#3773=DIRECTION ( 'NONE',  ( -1.000000000000000000, 0.000000000000000000, 0.000000000000000000 ) ) ;
#3783=EDGE_CURVE ( 'NONE', #15733, #27081, #7382, .T. ) ;
#3793=EDGE_CURVE ( 'NONE', #14835, #24556, #25486, .T. ) ;
#3835=ORIENTED_EDGE ( 'NONE', *, *, #12388, .T. ) ;
#3837=CARTESIAN_POINT ( 'NONE',  ( 8.000000000000000000, 16.92083251265334098, -4.460989585140788805 ) ) ;
#3856=AXIS2_PLACEMENT_3D ( 'NONE', #23588, #4164, #23041 ) ;
#3859=VECTOR ( 'NONE', #13553, 1000.000000000000000 ) ;
#3862=EDGE_CURVE ( 'NONE', #34739, #35010, #15810, .T. ) ;
#3863=CARTESIAN_POINT ( 'NONE',  ( 8.000000000000000000, 2.494040418455352182, 18.62763138773848937 ) ) ;
#3868=DIRECTION ( 'NONE',  ( 0.000000000000000000, 0.000000000000000000, 1.000000000000000000 ) ) ;
#3870=CARTESIAN_POINT ( 'NONE',  ( 0.000000000000000000, -11.06713717293248855, 13.55483219355725844 ) ) ;
#3887=AXIS2_PLACEMENT_3D ( 'NONE', #13127, #32366, #10236 ) ;
#3892=CYLINDRICAL_SURFACE ( 'NONE', #27210, 22.00000000000000000 ) ;
#3899=FACE_OUTER_BOUND ( 'NONE', #27076, .T. ) ;
#3913=DIRECTION ( 'NONE',  ( 0.000000000000000000, -1.000000000000000000, 0.000000000000000000 ) ) ;
#3915=ORIENTED_EDGE ( 'NONE', *, *, #34549, .F. ) ;
#3929=AXIS2_PLACEMENT_3D ( 'NONE', #18404, #4214, #29406 ) ;
#3949=DIRECTION ( 'NONE',  ( 0.000000000000000000, 0.000000000000000000, 1.000000000000000000 ) ) ;
#3968=AXIS2_PLACEMENT_3D ( 'NONE', #33944, #20053, #805 ) ;
#3973=CARTESIAN_POINT ( 'NONE',  ( 8.000000000000000000, -18.62763138773852134, 2.494040418455287345 ) ) ;
#3974=ORIENTED_EDGE ( 'NONE', *, *, #3455, .F. ) ;
#3985=DIRECTION ( 'NONE',  ( 0.000000000000000000, 0.000000000000000000, 1.000000000000000000 ) ) ;
#3995=ADVANCED_FACE ( 'NONE', ( #27543 ), #25364, .T. ) ;
#4006=EDGE_CURVE ( 'NONE', #34436, #17571, #35292, .T. ) ;
#4038=CARTESIAN_POINT ( 'NONE',  ( 8.000000000000000000, 19.83898331853701080, -9.508666619816441568 ) ) ;
#4049=LINE ( 'NONE', #7251, #31390 ) ;
#4073=AXIS2_PLACEMENT_3D ( 'NONE', #16633, #27647, #35216 ) ;
#4105=CARTESIAN_POINT ( 'NONE',  ( 8.000000000000000000, -16.53603053422215297, 8.931325931664547468 ) ) ;
#4106=CYLINDRICAL_SURFACE ( 'NONE', #7372, 8.000000000000001776 ) ;
#4117=DIRECTION ( 'NONE',  ( -1.000000000000000000, 0.000000000000000000, 0.000000000000000000 ) ) ;
#4118=DIRECTION ( 'NONE',  ( 0.000000000000000000, 0.000000000000000000, 1.000000000000000000 ) ) ;
#4120=DIRECTION ( 'NONE',  ( 0.000000000000000000, 0.9510565162951523099, 0.3090169943749513926 ) ) ;
#4121=CARTESIAN_POINT ( 'NONE',  ( 8.000000000000000000, -18.48663108841361336, 3.384281271887747078 ) ) ;
#4147=EDGE_LOOP ( 'NONE', ( #20861, #5933, #23613, #20709 ) ) ;
#4150=EDGE_CURVE ( 'NONE', #34739, #8636, #26079, .T. ) ;
#4157=DIRECTION ( 'NONE',  ( -1.000000000000000000, 0.000000000000000000, 0.000000000000000000 ) ) ;
#4164=DIRECTION ( 'NONE',  ( -1.000000000000000000, 0.000000000000000000, 0.000000000000000000 ) ) ;
#4168=ORIENTED_EDGE ( 'NONE', *, *, #7385, .F. ) ;
#4171=CIRCLE ( 'NONE', #12797, 8.000000000000010658 ) ;
#4187=VERTEX_POINT ( 'NONE', #19920 ) ;
#4201=AXIS2_PLACEMENT_3D ( 'NONE', #28271, #13396, #14390 ) ;
#4214=DIRECTION ( 'NONE',  ( -1.000000000000000000, 0.000000000000000000, 0.000000000000000000 ) ) ;
#4218=CARTESIAN_POINT ( 'NONE',  ( 0.000000000000000000, 0.000000000000000000, 0.000000000000000000 ) ) ;
#4268=VECTOR ( 'NONE', #34963, 1000.000000000000000 ) ;
#4294=DIRECTION ( 'NONE',  ( 0.000000000000000000, 0.000000000000000000, 1.000000000000000000 ) ) ;
#4295=DIRECTION ( 'NONE',  ( -1.000000000000000000, 0.000000000000000000, 0.000000000000000000 ) ) ;
#4313=ORIENTED_EDGE ( 'NONE', *, *, #19839, .F. ) ;
#4339=VERTEX_POINT ( 'NONE', #30370 ) ;
#4341=CLOSED_SHELL ( 'NONE', ( #15947, #18099, #19316, #32509, #18270, #5524, #23984, #12345, #27807, #24043, #7928, #975, #16730, #24465, #13654, #21232, #1164, #30955, #2434, #8183, #31657, #7895, #33089, #511, #18722, #25890, #18884, #7023, #24106, #20664, #10368, #24900, #12930, #30914, #21392, #35532, #9898, #1569, #1883, #17817, #474, #22257, #31944, #27045, #33202, #27359, #2226, #32157, #10560, #32236, #9717, #3995, #24227, #9692, #13176, #8376, #1531, #12770, #35487, #19836, #6253, #21481, #27394, #2930, #8670, #3081, #8395, #10188, #7862, #19008, #15984, #28928, #21626, #2649, #24284, #26014, #31120, #8427, #20430, #29278, #25812, #22253, #32809, #8602, #20944, #13496, #27582, #25983, #16183, #27694, #33548, #20396, #30886 ) ) ;
#4346=VERTEX_POINT ( 'NONE', #30189 ) ;
#4352=EDGE_CURVE ( 'NONE', #18803, #19338, #3365, .T. ) ;
#4385=CARTESIAN_POINT ( 'NONE',  ( 8.000000000000000000, 0.000000000000000000, 0.000000000000000000 ) ) ;
#4416=CARTESIAN_POINT ( 'NONE',  ( 0.000000000000000000, 0.000000000000000000, 17.49900000000000233 ) ) ;
#4421=EDGE_CURVE ( 'NONE', #31693, #27894, #26683, .T. ) ;
#4422=AXIS2_PLACEMENT_3D ( 'NONE', #15775, #15426, #18667 ) ;
#4437=CARTESIAN_POINT ( 'NONE',  ( 0.000000000000000000, 0.000000000000000000, 0.000000000000000000 ) ) ;
#4441=ORIENTED_EDGE ( 'NONE', *, *, #30217, .T. ) ;
#4442=EDGE_CURVE ( 'NONE', #8092, #24798, #3707, .T. ) ;
#4447=VERTEX_POINT ( 'NONE', #9636 ) ;
#4484=CIRCLE ( 'NONE', #7339, 17.49900000000001299 ) ;
#4486=DIRECTION ( 'NONE',  ( 0.000000000000000000, 1.000000000000000000, 3.491564676272318479E-15 ) ) ;
#4489=DIRECTION ( 'NONE',  ( 0.000000000000000000, 0.000000000000000000, 1.000000000000000000 ) ) ;
#4497=DIRECTION ( 'NONE',  ( -1.000000000000000000, 0.000000000000000000, 0.000000000000000000 ) ) ;
#4516=ORIENTED_EDGE ( 'NONE', *, *, #10844, .T. ) ;
#4540=EDGE_CURVE ( 'NONE', #4447, #27214, #6528, .T. ) ;
#4551=ORIENTED_EDGE ( 'NONE', *, *, #22256, .T. ) ;
#4556=EDGE_LOOP ( 'NONE', ( #9217, #22059, #5444, #24711 ) ) ;
#4566=ORIENTED_EDGE ( 'NONE', *, *, #20245, .F. ) ;
#4583=CIRCLE ( 'NONE', #1687, 8.000000000000007105 ) ;
#4601=DIRECTION ( 'NONE',  ( -1.000000000000000000, 0.000000000000000000, 0.000000000000000000 ) ) ;
#4602=EDGE_CURVE ( 'NONE', #21628, #15307, #10523, .T. ) ;
#4605=EDGE_CURVE ( 'NONE', #16930, #3480, #31848, .T. ) ;
#4611=EDGE_CURVE ( 'NONE', #23058, #16592, #11143, .T. ) ;
#4623=FACE_OUTER_BOUND ( 'NONE', #25068, .T. ) ;
#4629=ORIENTED_EDGE ( 'NONE', *, *, #21374, .F. ) ;
#4648=DIRECTION ( 'NONE',  ( 0.000000000000000000, 0.000000000000000000, 1.000000000000000000 ) ) ;
#4649=DIRECTION ( 'NONE',  ( 0.000000000000000000, 0.000000000000000000, 1.000000000000000000 ) ) ;
#4678=VERTEX_POINT ( 'NONE', #32477 ) ;
#4696=ORIENTED_EDGE ( 'NONE', *, *, #12263, .T. ) ;
#4710=DIRECTION ( 'NONE',  ( -1.000000000000000000, 0.000000000000000000, 0.000000000000000000 ) ) ;
#4713=VERTEX_POINT ( 'NONE', #18977 ) ;
#4717=ORIENTED_EDGE ( 'NONE', *, *, #22497, .T. ) ;
#4727=ORIENTED_EDGE ( 'NONE', *, *, #4150, .F. ) ;
#4750=CARTESIAN_POINT ( 'NONE',  ( 0.000000000000000000, 21.80633394113452539, 2.912696353505896063 ) ) ;
#4751=DIRECTION ( 'NONE',  ( -1.000000000000000000, 0.000000000000000000, 0.000000000000000000 ) ) ;
#4753=ORIENTED_EDGE ( 'NONE', *, *, #12466, .F. ) ;
#4766=VERTEX_POINT ( 'NONE', #33671 ) ;
#4800=CIRCLE ( 'NONE', #13425, 8.000000000000001776 ) ;
#4803=DIRECTION ( 'NONE',  ( -1.000000000000000000, 0.000000000000000000, 0.000000000000000000 ) ) ;
#4804=DIRECTION ( 'NONE',  ( 0.000000000000000000, 0.000000000000000000, 1.000000000000000000 ) ) ;
#4811=CYLINDRICAL_SURFACE ( 'NONE', #34415, 8.000000000000000000 ) ;
#4817=EDGE_LOOP ( 'NONE', ( #23966, #32613, #7392, #28962 ) ) ;
#4825=DIRECTION ( 'NONE',  ( -1.000000000000000000, 0.000000000000000000, 0.000000000000000000 ) ) ;
#4829=DIRECTION ( 'NONE',  ( -1.000000000000000000, 0.000000000000000000, 0.000000000000000000 ) ) ;
#4858=VECTOR ( 'NONE', #24661, 1000.000000000000000 ) ;
#4876=ORIENTED_EDGE ( 'NONE', *, *, #17833, .T. ) ;
#4881=VERTEX_POINT ( 'NONE', #17462 ) ;
#4885=AXIS2_PLACEMENT_3D ( 'NONE', #3231, #22470, #8610 ) ;
#4895=ORIENTED_EDGE ( 'NONE', *, *, #1547, .F. ) ;
#4918=DIRECTION ( 'NONE',  ( -1.000000000000000000, 0.000000000000000000, 0.000000000000000000 ) ) ;
#4923=CARTESIAN_POINT ( 'NONE',  ( 8.000000000000000000, -9.508666619816503740, -19.83898331853700014 ) ) ;
#4924=CARTESIAN_POINT ( 'NONE',  ( 0.000000000000000000, 3.384281271887823461, 18.48663108841358138 ) ) ;
#4934=EDGE_LOOP ( 'NONE', ( #8011, #7197, #29948, #581 ) ) ;
#4936=VECTOR ( 'NONE', #35385, 1000.000000000000000 ) ;
#4939=ORIENTED_EDGE ( 'NONE', *, *, #12357, .F. ) ;
#4941=AXIS2_PLACEMENT_3D ( 'NONE', #7301, #29096, #26397 ) ;
#4949=CARTESIAN_POINT ( 'NONE',  ( 8.000000000000000000, 17.47118961583601759, -0.9861715913088253682 ) ) ;
#4954=EDGE_CURVE ( 'NONE', #19206, #12602, #26128, .T. ) ;
#4970=DIRECTION ( 'NONE',  ( -1.000000000000000000, 0.000000000000000000, 0.000000000000000000 ) ) ;
#4977=LINE ( 'NONE', #10546, #28900 ) ;
#4992=CARTESIAN_POINT ( 'NONE',  ( 0.000000000000000000, -3.968388925834960723, 21.63912866391138934 ) ) ;
#4996=DIRECTION ( 'NONE',  ( 0.000000000000000000, 0.000000000000000000, 1.000000000000000000 ) ) ;
#5022=ORIENTED_EDGE ( 'NONE', *, *, #31954, .T. ) ;
#5026=DIRECTION ( 'NONE',  ( 0.000000000000000000, 0.8090169943749448977, 0.5877852522924766898 ) ) ;
#5031=EDGE_LOOP ( 'NONE', ( #18459, #29819, #13472, #32503 ) ) ;
#5048=CYLINDRICAL_SURFACE ( 'NONE', #15382, 22.00000000000000000 ) ;
#5058=ORIENTED_EDGE ( 'NONE', *, *, #34445, .T. ) ;
#5063=CARTESIAN_POINT ( 'NONE',  ( 8.000000000000000000, -4.460989585141086344, 16.92083251265324151 ) ) ;
#5067=AXIS2_PLACEMENT_3D ( 'NONE', #21520, #32886, #27669 ) ;
#5069=DIRECTION ( 'NONE',  ( -1.000000000000000000, 0.000000000000000000, 0.000000000000000000 ) ) ;
#5073=AXIS2_PLACEMENT_3D ( 'NONE', #8061, #3209, #14170 ) ;
#5080=EDGE_CURVE ( 'NONE', #16643, #30312, #18538, .T. ) ;
#5091=CARTESIAN_POINT ( 'NONE',  ( 4.000000000000003553, 3.968388925834817282, 21.63912866391139289 ) ) ;
#5101=DIRECTION ( 'NONE',  ( 0.000000000000000000, 0.9510565162951523099, 0.3090169943749513370 ) ) ;
#5103=EDGE_CURVE ( 'NONE', #9658, #16930, #817, .T. ) ;
#5118=ORIENTED_EDGE ( 'NONE', *, *, #26925, .F. ) ;
#5136=CARTESIAN_POINT ( 'NONE',  ( 0.000000000000000000, 0.000000000000000000, 0.000000000000000000 ) ) ;
#5137=EDGE_CURVE ( 'NONE', #33885, #18771, #32232, .T. ) ;
#5150=AXIS2_PLACEMENT_3D ( 'NONE', #16069, #24559, #35553 ) ;
#5152=DIRECTION ( 'NONE',  ( 0.000000000000000000, 0.000000000000000000, 1.000000000000000000 ) ) ;
#5154=DIRECTION ( 'NONE',  ( -1.000000000000000000, 0.000000000000000000, 0.000000000000000000 ) ) ;
#5162=ORIENTED_EDGE ( 'NONE', *, *, #25330, .F. ) ;
#5169=LINE ( 'NONE', #2116, #8557 ) ;
#5193=( NAMED_UNIT ( * ) PLANE_ANGLE_UNIT ( ) SI_UNIT ( $, .RADIAN. ) );
#5206=ORIENTED_EDGE ( 'NONE', *, *, #23066, .F. ) ;
#5215=LINE ( 'NONE', #18871, #17297 ) ;
#5244=DIRECTION ( 'NONE',  ( -1.000000000000000000, 0.000000000000000000, 0.000000000000000000 ) ) ;
#5246=ORIENTED_EDGE ( 'NONE', *, *, #18229, .T. ) ;
#5258=CYLINDRICAL_SURFACE ( 'NONE', #33978, 8.000000000000001776 ) ;
#5262=EDGE_CURVE ( 'NONE', #19686, #31127, #17495, .T. ) ;
#5278=FACE_OUTER_BOUND ( 'NONE', #24335, .T. ) ;
#5292=EDGE_LOOP ( 'NONE', ( #13744, #22570, #19434, #35394 ) ) ;
#5296=DIRECTION ( 'NONE',  ( -1.000000000000000000, 0.000000000000000000, 0.000000000000000000 ) ) ;
#5309=DIRECTION ( 'NONE',  ( -1.000000000000000000, 0.000000000000000000, 0.000000000000000000 ) ) ;
#5327=CARTESIAN_POINT ( 'NONE',  ( 8.000000000000000000, 0.000000000000000000, 0.000000000000000000 ) ) ;
#5331=DIRECTION ( 'NONE',  ( 0.000000000000000000, -0.9510565162951502005, -0.3090169943749580539 ) ) ;
#5349=DIRECTION ( 'NONE',  ( -1.000000000000000000, 0.000000000000000000, 0.000000000000000000 ) ) ;
#5380=VERTEX_POINT ( 'NONE', #7157 ) ;
#5396=CARTESIAN_POINT ( 'NONE',  ( -10.00000000000000178, 0.000000000000000000, 0.000000000000000000 ) ) ;
#5403=CARTESIAN_POINT ( 'NONE',  ( 0.000000000000000000, 5.400000000000021672, 1.000000000000001776 ) ) ;
#5414=AXIS2_PLACEMENT_3D ( 'NONE', #12024, #22995, #17584 ) ;
#5415=VERTEX_POINT ( 'NONE', #17772 ) ;
#5416=PLANE ( 'NONE',  #426 ) ;
#5425=ORIENTED_EDGE ( 'NONE', *, *, #19565, .F. ) ;
#5444=ORIENTED_EDGE ( 'NONE', *, *, #24880, .F. ) ;
#5446=DIRECTION ( 'NONE',  ( 0.000000000000000000, 0.000000000000000000, 1.000000000000000000 ) ) ;
#5462=ORIENTED_EDGE ( 'NONE', *, *, #17437, .T. ) ;
#5468=FACE_OUTER_BOUND ( 'NONE', #18827, .T. ) ;
#5477=DIRECTION ( 'NONE',  ( 0.000000000000000000, 0.000000000000000000, 1.000000000000000000 ) ) ;
#5499=CYLINDRICAL_SURFACE ( 'NONE', #34253, 17.49900000000000233 ) ;
#5523=EDGE_CURVE ( 'NONE', #3460, #24278, #8890, .T. ) ;
#5524=ADVANCED_FACE ( 'NONE', ( #31295 ), #12572, .F. ) ;
#5525=CARTESIAN_POINT ( 'NONE',  ( 4.000000000000003553, 10.46102064772339979, 19.35373470438986843 ) ) ;
#5536=EDGE_CURVE ( 'NONE', #30763, #32738, #10633, .T. ) ;
#5543=ORIENTED_EDGE ( 'NONE', *, *, #18986, .T. ) ;
#5558=ORIENTED_EDGE ( 'NONE', *, *, #30852, .T. ) ;
#5589=ORIENTED_EDGE ( 'NONE', *, *, #27567, .T. ) ;
#5590=ORIENTED_EDGE ( 'NONE', *, *, #33478, .F. ) ;
#5629=DIRECTION ( 'NONE',  ( -1.000000000000000000, 0.000000000000000000, 0.000000000000000000 ) ) ;
#5677=DIRECTION ( 'NONE',  ( 0.000000000000000000, 0.000000000000000000, 1.000000000000000000 ) ) ;
#5678=DIRECTION ( 'NONE',  ( 0.000000000000000000, 0.8090169943749490056, -0.5877852522924709167 ) ) ;
#5682=LINE ( 'NONE', #11428, #18182 ) ;
#5688=EDGE_LOOP ( 'NONE', ( #24189, #5820, #34328, #22516 ) ) ;
#5720=CIRCLE ( 'NONE', #25851, 17.49900000000001299 ) ;
#5722=VECTOR ( 'NONE', #8326, 1000.000000000000000 ) ;
#5736=VERTEX_POINT ( 'NONE', #8919 ) ;
#5746=DIRECTION ( 'NONE',  ( -1.000000000000000000, 0.000000000000000000, 0.000000000000000000 ) ) ;
#5753=ORIENTED_EDGE ( 'NONE', *, *, #11324, .F. ) ;
#5758=EDGE_CURVE ( 'NONE', #16380, #11959, #28488, .T. ) ;
#5761=ORIENTED_EDGE ( 'NONE', *, *, #11732, .T. ) ;
#5765=ORIENTED_EDGE ( 'NONE', *, *, #3783, .F. ) ;
#5781=CIRCLE ( 'NONE', #4073, 22.00000000000000000 ) ;
#5794=EDGE_LOOP ( 'NONE', ( #5590, #17220, #32767, #5753 ) ) ;
#5808=AXIS2_PLACEMENT_3D ( 'NONE', #23979, #32605, #32429 ) ;
#5820=ORIENTED_EDGE ( 'NONE', *, *, #14778, .T. ) ;
#5829=AXIS2_PLACEMENT_3D ( 'NONE', #3973, #20490, #23023 ) ;
#5835=CARTESIAN_POINT ( 'NONE',  ( 8.000000000000000000, 17.47118961583601759, -0.9861715913088253682 ) ) ;
#5836=CARTESIAN_POINT ( 'NONE',  ( 8.000000000000000000, 14.71414642875954648, 9.471478019455206621 ) ) ;
#5857=CIRCLE ( 'NONE', #13895, 8.000000000000007105 ) ;
#5894=CIRCLE ( 'NONE', #28930, 17.49900000000001654 ) ;
#5919=EDGE_CURVE ( 'NONE', #12842, #23201, #6045, .T. ) ;
#5929=ORIENTED_EDGE ( 'NONE', *, *, #17902, .T. ) ;
#5933=ORIENTED_EDGE ( 'NONE', *, *, #31405, .F. ) ;
#5936=CIRCLE ( 'NONE', #10542, 8.000000000000001776 ) ;
#5938=DIRECTION ( 'NONE',  ( 0.000000000000000000, 0.000000000000000000, 1.000000000000000000 ) ) ;
#5939=AXIS2_PLACEMENT_3D ( 'NONE', #33953, #8915, #34129 ) ;
#5947=AXIS2_PLACEMENT_3D ( 'NONE', #9413, #20739, #34629 ) ;
#5957=LINE ( 'NONE', #27922, #3312 ) ;
#5960=CIRCLE ( 'NONE', #12286, 8.000000000000007105 ) ;
#5963=VERTEX_POINT ( 'NONE', #11798 ) ;
#5984=VERTEX_POINT ( 'NONE', #26033 ) ;
#5989=ORIENTED_EDGE ( 'NONE', *, *, #28611, .F. ) ;
#6006=CYLINDRICAL_SURFACE ( 'NONE', #31275, 8.000000000000001776 ) ;
#6031=VERTEX_POINT ( 'NONE', #15921 ) ;
#6043=CARTESIAN_POINT ( 'NONE',  ( 0.000000000000000000, 14.71414642875953938, 9.471478019455203068 ) ) ;
#6045=CIRCLE ( 'NONE', #25021, 22.00000000000000000 ) ;
#6056=CARTESIAN_POINT ( 'NONE',  ( 4.000000000000003553, 10.46102064772367868, -19.35373470438974053 ) ) ;
#6062=ORIENTED_EDGE ( 'NONE', *, *, #724, .T. ) ;
#6077=AXIS2_PLACEMENT_3D ( 'NONE', #6163, #17128, #402 ) ;
#6083=AXIS2_PLACEMENT_3D ( 'NONE', #33457, #22635, #20109 ) ;
#6085=LINE ( 'NONE', #31281, #34598 ) ;
#6100=CARTESIAN_POINT ( 'NONE',  ( 0.000000000000000000, 13.60411018104320036, 12.96676809804154118 ) ) ;
#6134=EDGE_CURVE ( 'NONE', #11194, #12842, #18269, .T. ) ;
#6147=ORIENTED_EDGE ( 'NONE', *, *, #34625, .F. ) ;
#6160=CIRCLE ( 'NONE', #26290, 8.000000000000001776 ) ;
#6163=CARTESIAN_POINT ( 'NONE',  ( 8.000000000000000000, 0.000000000000000000, 0.000000000000000000 ) ) ;
#6169=EDGE_CURVE ( 'NONE', #4346, #14835, #10682, .T. ) ;
#6175=AXIS2_PLACEMENT_3D ( 'NONE', #18840, #24427, #8378 ) ;
#6181=CIRCLE ( 'NONE', #10224, 17.49900000000001654 ) ;
#6183=EDGE_CURVE ( 'NONE', #20524, #2111, #29076, .T. ) ;
#6191=ORIENTED_EDGE ( 'NONE', *, *, #10844, .F. ) ;
#6199=AXIS2_PLACEMENT_3D ( 'NONE', #4385, #9411, #7427 ) ;
#6207=EDGE_CURVE ( 'NONE', #19338, #1815, #1476, .T. ) ;
#6209=ORIENTED_EDGE ( 'NONE', *, *, #8034, .F. ) ;
#6228=CARTESIAN_POINT ( 'NONE',  ( 8.000000000000000000, 8.931325931664597206, 16.53603053422209612 ) ) ;
#6243=CARTESIAN_POINT ( 'NONE',  ( 8.000000000000000000, 0.000000000000000000, 17.49900000000000233 ) ) ;
#6249=CARTESIAN_POINT ( 'NONE',  ( 8.000000000000000000, 16.53603053422208902, -8.931325931664652273 ) ) ;
#6253=ADVANCED_FACE ( 'NONE', ( #33378 ), #430, .T. ) ;
#6259=ORIENTED_EDGE ( 'NONE', *, *, #18052, .F. ) ;
#6266=DIRECTION ( 'NONE',  ( 0.000000000000000000, -0.3090169943749545567, 0.9510565162951513107 ) ) ;
#6273=DIRECTION ( 'NONE',  ( -1.000000000000000000, 0.000000000000000000, 0.000000000000000000 ) ) ;
#6285=CARTESIAN_POINT ( 'NONE',  ( 0.000000000000000000, 0.000000000000000000, 0.000000000000000000 ) ) ;
#6299=ORIENTED_EDGE ( 'NONE', *, *, #34445, .F. ) ;
#6309=CARTESIAN_POINT ( 'NONE',  ( 8.000000000000000000, 6.336799421339808447, 16.31134495048485533 ) ) ;
#6311=DIRECTION ( 'NONE',  ( -1.000000000000000000, 0.000000000000000000, 0.000000000000000000 ) ) ;
#6326=EDGE_LOOP ( 'NONE', ( #7978, #10210, #21172, #28261 ) ) ;
#6331=ORIENTED_EDGE ( 'NONE', *, *, #5103, .T. ) ;
#6344=ORIENTED_EDGE ( 'NONE', *, *, #18491, .T. ) ;
#6345=DIRECTION ( 'NONE',  ( 0.000000000000000000, 0.000000000000000000, -1.000000000000000000 ) ) ;
#6358=CIRCLE ( 'NONE', #5808, 8.000000000000015987 ) ;
#6369=DIRECTION ( 'NONE',  ( -1.000000000000000000, 0.000000000000000000, 0.000000000000000000 ) ) ;
#6372=DIRECTION ( 'NONE',  ( 0.000000000000000000, 0.000000000000000000, 1.000000000000000000 ) ) ;
#6375=ORIENTED_EDGE ( 'NONE', *, *, #1207, .F. ) ;
#6391=EDGE_CURVE ( 'NONE', #1617, #15604, #23922, .T. ) ;
#6399=DIRECTION ( 'NONE',  ( 0.000000000000000000, 0.000000000000000000, 1.000000000000000000 ) ) ;
#6426=CARTESIAN_POINT ( 'NONE',  ( 0.000000000000000000, -16.53603053422215297, 8.931325931664547468 ) ) ;
#6454=ORIENTED_EDGE ( 'NONE', *, *, #14256, .T. ) ;
#6485=ORIENTED_EDGE ( 'NONE', *, *, #11730, .T. ) ;
#6495=VERTEX_POINT ( 'NONE', #11951 ) ;
#6505=ORIENTED_EDGE ( 'NONE', *, *, #13879, .T. ) ;
#6518=CIRCLE ( 'NONE', #1362, 8.000000000000001776 ) ;
#6522=CARTESIAN_POINT ( 'NONE',  ( 4.000000000000003553, -10.46102064772325413, -19.35373470438994659 ) ) ;
#6528=CIRCLE ( 'NONE', #9410, 8.000000000000007105 ) ;
#6532=CARTESIAN_POINT ( 'NONE',  ( -10.00000000000000178, 0.000000000000000000, 0.000000000000000000 ) ) ;
#6546=VERTEX_POINT ( 'NONE', #7431 ) ;
#6573=CIRCLE ( 'NONE', #16362, 8.000000000000003553 ) ;
#6603=EDGE_CURVE ( 'NONE', #8203, #32783, #33693, .T. ) ;
#6622=DIRECTION ( 'NONE',  ( -1.000000000000000000, 0.000000000000000000, 0.000000000000000000 ) ) ;
#6625=CARTESIAN_POINT ( 'NONE',  ( 8.000000000000000000, 16.94522934049215124, 8.128228055638924587 ) ) ;
#6627=VERTEX_POINT ( 'NONE', #23647 ) ;
#6645=ORIENTED_EDGE ( 'NONE', *, *, #28721, .F. ) ;
#6650=CARTESIAN_POINT ( 'NONE',  ( 8.000000000000000000, -11.06713717293229138, -13.55483219355740765 ) ) ;
#6658=AXIS2_PLACEMENT_3D ( 'NONE', #12488, #1689, #17874 ) ;
#6661=DIRECTION ( 'NONE',  ( 0.000000000000000000, 0.000000000000000000, 1.000000000000000000 ) ) ;
#6664=DIRECTION ( 'NONE',  ( 0.000000000000000000, 0.000000000000000000, -1.000000000000000000 ) ) ;
#6671=ORIENTED_EDGE ( 'NONE', *, *, #10411, .T. ) ;
#6710=FACE_OUTER_BOUND ( 'NONE', #1735, .T. ) ;
#6711=DIRECTION ( 'NONE',  ( 0.000000000000000000, -0.9510565162951500895, -0.3090169943749579429 ) ) ;
#6713=AXIS2_PLACEMENT_3D ( 'NONE', #1018, #30898, #34136 ) ;
#6722=CARTESIAN_POINT ( 'NONE',  ( 0.000000000000000000, -18.62763138773852134, 10.49404041845529001 ) ) ;
#6738=AXIS2_PLACEMENT_3D ( 'NONE', #5136, #10518, #21480 ) ;
#6748=FACE_OUTER_BOUND ( 'NONE', #14259, .T. ) ;
#6766=CIRCLE ( 'NONE', #24617, 22.00000000000000000 ) ;
#6778=DIRECTION ( 'NONE',  ( -1.000000000000000000, 0.000000000000000000, 0.000000000000000000 ) ) ;
#6795=CYLINDRICAL_SURFACE ( 'NONE', #11706, 4.000000000000000000 ) ;
#6809=ORIENTED_EDGE ( 'NONE', *, *, #25817, .T. ) ;
#6816=EDGE_CURVE ( 'NONE', #26672, #8935, #2938, .T. ) ;
#6842=CYLINDRICAL_SURFACE ( 'NONE', #17058, 8.000000000000000000 ) ;
#6859=EDGE_CURVE ( 'NONE', #30484, #20884, #22790, .T. ) ;
#6924=VECTOR ( 'NONE', #35577, 1000.000000000000000 ) ;
#6931=ORIENTED_EDGE ( 'NONE', *, *, #22741, .F. ) ;
#6935=DIRECTION ( 'NONE',  ( 0.000000000000000000, -1.000000000000000000, -1.040834085586082363E-14 ) ) ;
#6964=ORIENTED_EDGE ( 'NONE', *, *, #4954, .F. ) ;
#6981=EDGE_LOOP ( 'NONE', ( #33654, #10938, #19775, #35610 ) ) ;
#7010=DIRECTION ( 'NONE',  ( -1.000000000000000000, 0.000000000000000000, 0.000000000000000000 ) ) ;
#7022=ORIENTED_EDGE ( 'NONE', *, *, #21144, .F. ) ;
#7023=ADVANCED_FACE ( 'NONE', ( #25421 ), #920, .T. ) ;
#7033=ORIENTED_EDGE ( 'NONE', *, *, #12221, .F. ) ;
#7047=AXIS2_PLACEMENT_3D ( 'NONE', #25978, #15146, #7056 ) ;
#7056=DIRECTION ( 'NONE',  ( 0.000000000000000000, 0.000000000000000000, 1.000000000000000000 ) ) ;
#7079=DIRECTION ( 'NONE',  ( -1.000000000000000000, 0.000000000000000000, 0.000000000000000000 ) ) ;
#7081=CARTESIAN_POINT ( 'NONE',  ( 8.000000000000000000, -2.494040418455483188, 18.62763138773849292 ) ) ;
#7087=ORIENTED_EDGE ( 'NONE', *, *, #22857, .F. ) ;
#7090=EDGE_CURVE ( 'NONE', #24162, #17966, #7204, .T. ) ;
#7107=LINE ( 'NONE', #29269, #7857 ) ;
#7108=DIRECTION ( 'NONE',  ( -1.000000000000000000, 0.000000000000000000, 0.000000000000000000 ) ) ;
#7110=CIRCLE ( 'NONE', #9400, 8.000000000000010658 ) ;
#7117=VERTEX_POINT ( 'NONE', #20695 ) ;
#7132=CARTESIAN_POINT ( 'NONE',  ( 8.000000000000000000, 0.000000000000000000, 0.000000000000000000 ) ) ;
#7133=ORIENTED_EDGE ( 'NONE', *, *, #28721, .T. ) ;
#7147=AXIS2_PLACEMENT_3D ( 'NONE', #28964, #9867, #20476 ) ;
#7150=DIRECTION ( 'NONE',  ( -1.000000000000000000, 0.000000000000000000, 0.000000000000000000 ) ) ;
#7157=CARTESIAN_POINT ( 'NONE',  ( 8.000000000000000000, 3.968388925835109049, -21.63912866391136447 ) ) ;
#7167=CARTESIAN_POINT ( 'NONE',  ( 8.000000000000000000, 9.471478019455140895, 14.71414642875960332 ) ) ;
#7186=LINE ( 'NONE', #6522, #3514 ) ;
#7190=DIRECTION ( 'NONE',  ( -1.000000000000000000, 0.000000000000000000, 0.000000000000000000 ) ) ;
#7197=ORIENTED_EDGE ( 'NONE', *, *, #1207, .T. ) ;
#7204=LINE ( 'NONE', #32533, #21066 ) ;
#7239=CARTESIAN_POINT ( 'NONE',  ( 0.000000000000000000, 3.968388925834817282, 21.63912866391139289 ) ) ;
#7242=FACE_OUTER_BOUND ( 'NONE', #4147, .T. ) ;
#7251=CARTESIAN_POINT ( 'NONE',  ( 8.000000000000000000, 17.47118961583601759, 0.9861715913088272556 ) ) ;
#7254=AXIS2_PLACEMENT_3D ( 'NONE', #31823, #10408, #2320 ) ;
#7283=AXIS2_PLACEMENT_3D ( 'NONE', #22564, #258, #5678 ) ;
#7285=DIRECTION ( 'NONE',  ( 0.000000000000000000, 0.000000000000000000, -1.000000000000000000 ) ) ;
#7295=CARTESIAN_POINT ( 'NONE',  ( 8.000000000000000000, -8.128228055638974325, 16.94522934049209795 ) ) ;
#7301=CARTESIAN_POINT ( 'NONE',  ( 8.000000000000000000, 0.000000000000000000, 0.000000000000000000 ) ) ;
#7304=CIRCLE ( 'NONE', #21088, 17.49900000000002720 ) ;
#7309=ORIENTED_EDGE ( 'NONE', *, *, #30598, .F. ) ;
#7314=AXIS2_PLACEMENT_3D ( 'NONE', #20806, #9675, #28939 ) ;
#7327=DIRECTION ( 'NONE',  ( -1.000000000000000000, 0.000000000000000000, 0.000000000000000000 ) ) ;
#7328=CARTESIAN_POINT ( 'NONE',  ( 0.000000000000000000, 0.000000000000000000, 0.000000000000000000 ) ) ;
#7329=VERTEX_POINT ( 'NONE', #14152 ) ;
#7339=AXIS2_PLACEMENT_3D ( 'NONE', #19358, #30366, #27496 ) ;
#7347=EDGE_CURVE ( 'NONE', #24556, #7742, #21091, .T. ) ;
#7349=DIRECTION ( 'NONE',  ( -1.000000000000000000, 0.000000000000000000, 0.000000000000000000 ) ) ;
#7352=VECTOR ( 'NONE', #19436, 1000.000000000000000 ) ;
#7353=DIRECTION ( 'NONE',  ( 0.000000000000000000, 0.000000000000000000, 1.000000000000000000 ) ) ;
#7357=DIRECTION ( 'NONE',  ( -1.000000000000000000, 0.000000000000000000, 0.000000000000000000 ) ) ;
#7372=AXIS2_PLACEMENT_3D ( 'NONE', #33605, #12009, #31096 ) ;
#7380=CARTESIAN_POINT ( 'NONE',  ( 0.000000000000000000, 10.46102064772339979, 19.35373470438986843 ) ) ;
#7382=LINE ( 'NONE', #15994, #16253 ) ;
#7384=CARTESIAN_POINT ( 'NONE',  ( 8.000000000000000000, 0.000000000000000000, 0.000000000000000000 ) ) ;
#7385=EDGE_CURVE ( 'NONE', #17296, #12175, #19380, .T. ) ;
#7391=EDGE_CURVE ( 'NONE', #12602, #25795, #22252, .T. ) ;
#7392=ORIENTED_EDGE ( 'NONE', *, *, #20073, .F. ) ;
#7413=DIRECTION ( 'NONE',  ( -1.000000000000000000, 0.000000000000000000, 0.000000000000000000 ) ) ;
#7427=DIRECTION ( 'NONE',  ( 0.000000000000000000, 0.000000000000000000, 1.000000000000000000 ) ) ;
#7428=DIRECTION ( 'NONE',  ( 0.000000000000000000, 0.000000000000000000, 1.000000000000000000 ) ) ;
#7431=CARTESIAN_POINT ( 'NONE',  ( 8.000000000000000000, -9.471478019455243924, 14.71414642875952161 ) ) ;
#7434=AXIS2_PLACEMENT_3D ( 'NONE', #7328, #18300, #4649 ) ;
#7435=EDGE_CURVE ( 'NONE', #14850, #29835, #23394, .T. ) ;
#7451=DIRECTION ( 'NONE',  ( -1.000000000000000000, 0.000000000000000000, 0.000000000000000000 ) ) ;
#7462=ORIENTED_EDGE ( 'NONE', *, *, #30839, .F. ) ;
#7468=CARTESIAN_POINT ( 'NONE',  ( 8.000000000000000000, -10.46102064772354723, 19.35373470438981514 ) ) ;
#7470=ORIENTED_EDGE ( 'NONE', *, *, #33855, .T. ) ;
#7473=CYLINDRICAL_SURFACE ( 'NONE', #26285, 17.49900000000000233 ) ;
#7489=LINE ( 'NONE', #18472, #11422 ) ;
#7507=EDGE_CURVE ( 'NONE', #21532, #30052, #34932, .T. ) ;
#7537=EDGE_LOOP ( 'NONE', ( #5246, #24816, #31177, #11344 ) ) ;
#7554=DIRECTION ( 'NONE',  ( -1.000000000000000000, 0.000000000000000000, 0.000000000000000000 ) ) ;
#7569=EDGE_LOOP ( 'NONE', ( #25841, #3656, #2365, #21582 ) ) ;
#7578=CARTESIAN_POINT ( 'NONE',  ( -10.00000000000000178, 0.000000000000000000, 0.000000000000000000 ) ) ;
#7614=CARTESIAN_POINT ( 'NONE',  ( 0.000000000000000000, 5.399999999999999467, -1.000000000000003109 ) ) ;
#7620=DIRECTION ( 'NONE',  ( 0.000000000000000000, 0.000000000000000000, 1.000000000000000000 ) ) ;
#7629=DIRECTION ( 'NONE',  ( -1.000000000000000000, 0.000000000000000000, 0.000000000000000000 ) ) ;
#7642=FACE_OUTER_BOUND ( 'NONE', #11501, .T. ) ;
#7654=ORIENTED_EDGE ( 'NONE', *, *, #30217, .F. ) ;
#7656=ORIENTED_EDGE ( 'NONE', *, *, #8445, .F. ) ;
#7668=FACE_BOUND ( 'NONE', #24588, .T. ) ;
#7671=LINE ( 'NONE', #2476, #28031 ) ;
#7679=CARTESIAN_POINT ( 'NONE',  ( 0.000000000000000000, 0.000000000000000000, 0.000000000000000000 ) ) ;
#7680=CARTESIAN_POINT ( 'NONE',  ( 8.000000000000000000, 16.31134495048494060, -6.336799421339643246 ) ) ;
#7704=ORIENTED_EDGE ( 'NONE', *, *, #14731, .T. ) ;
#7724=AXIS2_PLACEMENT_3D ( 'NONE', #25632, #25816, #31021 ) ;
#7730=ORIENTED_EDGE ( 'NONE', *, *, #24865, .T. ) ;
#7742=VERTEX_POINT ( 'NONE', #768 ) ;
#7754=ORIENTED_EDGE ( 'NONE', *, *, #25760, .T. ) ;
#7756=CARTESIAN_POINT ( 'NONE',  ( 8.000000000000000000, -3.384281271887945586, 18.48663108841355651 ) ) ;
#7769=CARTESIAN_POINT ( 'NONE',  ( 0.000000000000000000, 0.000000000000000000, 0.000000000000000000 ) ) ;
#7793=AXIS2_PLACEMENT_3D ( 'NONE', #25815, #9942, #9406 ) ;
#7815=DIRECTION ( 'NONE',  ( 0.000000000000000000, 0.000000000000000000, 1.000000000000000000 ) ) ;
#7833=CARTESIAN_POINT ( 'NONE',  ( 8.000000000000000000, 0.000000000000000000, 0.000000000000000000 ) ) ;
#7842=AXIS2_PLACEMENT_3D ( 'NONE', #33497, #19784, #30799 ) ;
#7857=VECTOR ( 'NONE', #26569, 1000.000000000000000 ) ;
#7859=CIRCLE ( 'NONE', #9592, 17.49900000000001299 ) ;
#7861=DIRECTION ( 'NONE',  ( -1.000000000000000000, 0.000000000000000000, 0.000000000000000000 ) ) ;
#7862=ADVANCED_FACE ( 'NONE', ( #26426 ), #34894, .T. ) ;
#7882=DIRECTION ( 'NONE',  ( -1.000000000000000000, 0.000000000000000000, 0.000000000000000000 ) ) ;
#7892=ORIENTED_EDGE ( 'NONE', *, *, #17976, .T. ) ;
#7895=ADVANCED_FACE ( 'NONE', ( #28941 ), #15058, .T. ) ;
#7898=AXIS2_PLACEMENT_3D ( 'NONE', #15488, #18381, #29382 ) ;
#7902=DIRECTION ( 'NONE',  ( 1.000000000000000000, -0.000000000000000000, -0.000000000000000000 ) ) ;
#7905=CIRCLE ( 'NONE', #28046, 22.00000000000000000 ) ;
#7910=DIRECTION ( 'NONE',  ( -1.000000000000000000, 0.000000000000000000, 0.000000000000000000 ) ) ;
#7918=AXIS2_PLACEMENT_3D ( 'NONE', #16397, #13200, #21811 ) ;
#7919=EDGE_LOOP ( 'NONE', ( #16845, #26912, #1881, #16569 ) ) ;
#7921=DIRECTION ( 'NONE',  ( 0.000000000000000000, -1.000000000000000000, 0.000000000000000000 ) ) ;
#7928=ADVANCED_FACE ( 'NONE', ( #20807 ), #29842, .T. ) ;
#7936=DIRECTION ( 'NONE',  ( 0.000000000000000000, 0.000000000000000000, -1.000000000000000000 ) ) ;
#7940=DIRECTION ( 'NONE',  ( -1.000000000000000000, 0.000000000000000000, 0.000000000000000000 ) ) ;
#7954=VERTEX_POINT ( 'NONE', #15952 ) ;
#7978=ORIENTED_EDGE ( 'NONE', *, *, #17902, .F. ) ;
#7988=EDGE_CURVE ( 'NONE', #29170, #2115, #9048, .T. ) ;
#7989=DIRECTION ( 'NONE',  ( -1.000000000000000000, 0.000000000000000000, 0.000000000000000000 ) ) ;
#7993=DIRECTION ( 'NONE',  ( -1.000000000000000000, 0.000000000000000000, 0.000000000000000000 ) ) ;
#7994=EDGE_CURVE ( 'NONE', #1847, #33885, #29756, .T. ) ;
#8007=DIRECTION ( 'NONE',  ( -1.000000000000000000, 0.000000000000000000, 0.000000000000000000 ) ) ;
#8009=FACE_OUTER_BOUND ( 'NONE', #27018, .T. ) ;
#8011=ORIENTED_EDGE ( 'NONE', *, *, #10778, .T. ) ;
#8031=CARTESIAN_POINT ( 'NONE',  ( 8.000000000000000000, 0.000000000000000000, 0.000000000000000000 ) ) ;
#8034=EDGE_CURVE ( 'NONE', #27440, #30478, #8104, .T. ) ;
#8059=AXIS2_PLACEMENT_3D ( 'NONE', #14029, #17562, #25026 ) ;
#8061=CARTESIAN_POINT ( 'NONE',  ( 8.000000000000000000, 0.000000000000000000, 0.000000000000000000 ) ) ;
#8067=DIRECTION ( 'NONE',  ( 1.000000000000000000, -0.000000000000000000, 0.000000000000000000 ) ) ;
#8069=ORIENTED_EDGE ( 'NONE', *, *, #28275, .T. ) ;
#8084=DIRECTION ( 'NONE',  ( 0.000000000000000000, 0.000000000000000000, -1.000000000000000000 ) ) ;
#8085=CARTESIAN_POINT ( 'NONE',  ( 8.000000000000000000, -14.71414642875948608, -9.471478019455300768 ) ) ;
#8086=ORIENTED_EDGE ( 'NONE', *, *, #19839, .T. ) ;
#8092=VERTEX_POINT ( 'NONE', #33576 ) ;
#8104=CIRCLE ( 'NONE', #28803, 22.00000000000000000 ) ;
#8106=DIRECTION ( 'NONE',  ( 0.000000000000000000, 0.000000000000000000, 1.000000000000000000 ) ) ;
#8121=CYLINDRICAL_SURFACE ( 'NONE', #34381, 22.00000000000000000 ) ;
#8124=CARTESIAN_POINT ( 'NONE',  ( 0.000000000000000000, 15.92965478239641008, -15.17386234660366284 ) ) ;
#8152=EDGE_CURVE ( 'NONE', #5415, #27865, #5957, .T. ) ;
#8154=VECTOR ( 'NONE', #21438, 1000.000000000000000 ) ;
#8157=FACE_OUTER_BOUND ( 'NONE', #27335, .T. ) ;
#8178=CARTESIAN_POINT ( 'NONE',  ( 0.000000000000000000, 16.31134495048485178, 6.336799421339877725 ) ) ;
#8183=ADVANCED_FACE ( 'NONE', ( #32800 ), #8121, .T. ) ;
#8184=ORIENTED_EDGE ( 'NONE', *, *, #23202, .T. ) ;
#8186=SHAPE_REPRESENTATION ( 'spur gear_iso_ISO - Spur gear 2M 20T 20PA 8FW ---S20A75H50L8.0S1', ( #21307 ), #30547 ) ;
#8196=VECTOR ( 'NONE', #28328, 1000.000000000000000 ) ;
#8203=VERTEX_POINT ( 'NONE', #6309 ) ;
#8234=ORIENTED_EDGE ( 'NONE', *, *, #24865, .F. ) ;
#8247=DIRECTION ( 'NONE',  ( 0.000000000000000000, -0.3090169943749546677, 0.9510565162951511997 ) ) ;
#8281=CARTESIAN_POINT ( 'NONE',  ( 4.000000000000003553, 19.35373470438998211, -10.46102064772319729 ) ) ;
#8297=EDGE_LOOP ( 'NONE', ( #2862, #573, #20752, #12298 ) ) ;
#8298=ORIENTED_EDGE ( 'NONE', *, *, #21808, .F. ) ;
#8300=FACE_OUTER_BOUND ( 'NONE', #27249, .T. ) ;
#8303=CARTESIAN_POINT ( 'NONE',  ( 8.000000000000000000, -16.31134495048480559, -6.336799421339987859 ) ) ;
#8311=CARTESIAN_POINT ( 'NONE',  ( 0.000000000000000000, 6.071532165918824830E-15, 1.000000000000000000 ) ) ;
#8326=DIRECTION ( 'NONE',  ( -1.000000000000000000, 0.000000000000000000, 0.000000000000000000 ) ) ;
#8349=DIRECTION ( 'NONE',  ( 1.000000000000000000, -0.000000000000000000, -0.000000000000000000 ) ) ;
#8371=AXIS2_PLACEMENT_3D ( 'NONE', #4218, #3503, #1318 ) ;
#8376=ADVANCED_FACE ( 'NONE', ( #24307 ), #1988, .T. ) ;
#8378=DIRECTION ( 'NONE',  ( 0.000000000000000000, -0.9510565162951565288, 0.3090169943749384029 ) ) ;
#8380=VECTOR ( 'NONE', #3913, 1000.000000000000000 ) ;
#8395=ADVANCED_FACE ( 'NONE', ( #9892 ), #34947, .T. ) ;
#8396=EDGE_CURVE ( 'NONE', #23042, #14072, #29134, .T. ) ;
#8417=CIRCLE ( 'NONE', #17014, 8.000000000000003553 ) ;
#8427=ADVANCED_FACE ( 'NONE', ( #21573 ), #15812, .T. ) ;
#8432=DIRECTION ( 'NONE',  ( 0.000000000000000000, 0.000000000000000000, 1.000000000000000000 ) ) ;
#8442=ORIENTED_EDGE ( 'NONE', *, *, #11324, .T. ) ;
#8445=EDGE_CURVE ( 'NONE', #29017, #29018, #13156, .T. ) ;
#8459=AXIS2_PLACEMENT_3D ( 'NONE', #35199, #10697, #13758 ) ;
#8468=ORIENTED_EDGE ( 'NONE', *, *, #16956, .T. ) ;
#8494=ORIENTED_EDGE ( 'NONE', *, *, #33317, .F. ) ;
#8540=ORIENTED_EDGE ( 'NONE', *, *, #23757, .F. ) ;
#8541=CIRCLE ( 'NONE', #5150, 22.00000000000000000 ) ;
#8548=ORIENTED_EDGE ( 'NONE', *, *, #7090, .F. ) ;
#8557=VECTOR ( 'NONE', #13096, 1000.000000000000000 ) ;
#8592=CARTESIAN_POINT ( 'NONE',  ( 0.000000000000000000, -18.62763138773848581, -2.494040418455559127 ) ) ;
#8596=ORIENTED_EDGE ( 'NONE', *, *, #6169, .T. ) ;
#8602=ADVANCED_FACE ( 'NONE', ( #19419 ), #30417, .T. ) ;
#8604=DIRECTION ( 'NONE',  ( 0.000000000000000000, 0.000000000000000000, 1.000000000000000000 ) ) ;
#8608=CIRCLE ( 'NONE', #1173, 22.00000000000000000 ) ;
#8610=DIRECTION ( 'NONE',  ( 0.000000000000000000, 0.000000000000000000, -1.000000000000000000 ) ) ;
#8636=VERTEX_POINT ( 'NONE', #2532 ) ;
#8659=CARTESIAN_POINT ( 'NONE',  ( 0.000000000000000000, -13.55483219355720337, -11.06713717293254362 ) ) ;
#8670=ADVANCED_FACE ( 'NONE', ( #22292 ), #10974, .T. ) ;
#8671=ORIENTED_EDGE ( 'NONE', *, *, #197, .F. ) ;
#8672=EDGE_CURVE ( 'NONE', #27894, #21954, #14190, .T. ) ;
#8685=ORIENTED_EDGE ( 'NONE', *, *, #8152, .F. ) ;
#8700=FACE_OUTER_BOUND ( 'NONE', #10948, .T. ) ;
#8701=ORIENTED_EDGE ( 'NONE', *, *, #26688, .F. ) ;
#8706=PLANE ( 'NONE',  #20438 ) ;
#8712=DIRECTION ( 'NONE',  ( -1.000000000000000000, 0.000000000000000000, 0.000000000000000000 ) ) ;
#8716=VECTOR ( 'NONE', #12647, 1000.000000000000000 ) ;
#8721=EDGE_CURVE ( 'NONE', #1074, #18771, #7859, .T. ) ;
#8730=VECTOR ( 'NONE', #26778, 1000.000000000000000 ) ;
#8735=CARTESIAN_POINT ( 'NONE',  ( 8.000000000000000000, 0.000000000000000000, 0.000000000000000000 ) ) ;
#8738=DIRECTION ( 'NONE',  ( 0.000000000000000000, 0.5877852522924682521, 0.8090169943749511150 ) ) ;
#8775=DIRECTION ( 'NONE',  ( 0.000000000000000000, 0.000000000000000000, 1.000000000000000000 ) ) ;
#8786=ORIENTED_EDGE ( 'NONE', *, *, #17935, .T. ) ;
#8788=DIRECTION ( 'NONE',  ( 0.000000000000000000, 0.9510565162951544194, -0.3090169943749449533 ) ) ;
#8800=CARTESIAN_POINT ( 'NONE',  ( 8.000000000000000000, 0.000000000000000000, 0.000000000000000000 ) ) ;
#8802=ORIENTED_EDGE ( 'NONE', *, *, #30564, .T. ) ;
#8848=ORIENTED_EDGE ( 'NONE', *, *, #16902, .T. ) ;
#8855=ORIENTED_EDGE ( 'NONE', *, *, #19173, .T. ) ;
#8860=ORIENTED_EDGE ( 'NONE', *, *, #29343, .T. ) ;
#8890=CIRCLE ( 'NONE', #16921, 8.000000000000001776 ) ;
#8905=CARTESIAN_POINT ( 'NONE',  ( 4.000000000000003553, 21.80633394113450052, -2.912696353505896063 ) ) ;
#8909=EDGE_CURVE ( 'NONE', #29036, #26218, #7304, .T. ) ;
#8915=DIRECTION ( 'NONE',  ( -1.000000000000000000, 0.000000000000000000, 0.000000000000000000 ) ) ;
#8918=DIRECTION ( 'NONE',  ( -1.000000000000000000, 0.000000000000000000, 0.000000000000000000 ) ) ;
#8919=CARTESIAN_POINT ( 'NONE',  ( 8.000000000000000000, -16.31134495048487310, 6.336799421339755156 ) ) ;
#8935=VERTEX_POINT ( 'NONE', #34712 ) ;
#8942=ORIENTED_EDGE ( 'NONE', *, *, #25274, .T. ) ;
#8968=DIRECTION ( 'NONE',  ( 0.000000000000000000, 0.8090169943749490056, -0.5877852522924709167 ) ) ;
#8973=CIRCLE ( 'NONE', #9549, 8.000000000000001776 ) ;
#8994=VECTOR ( 'NONE', #24587, 1000.000000000000000 ) ;
#8998=CIRCLE ( 'NONE', #26268, 8.000000000000015987 ) ;
#9009=VERTEX_POINT ( 'NONE', #13115 ) ;
#9015=EDGE_CURVE ( 'NONE', #6495, #5380, #13051, .T. ) ;
#9016=VECTOR ( 'NONE', #23182, 1000.000000000000000 ) ;
#9020=AXIS2_PLACEMENT_3D ( 'NONE', #32667, #5309, #5477 ) ;
#9043=VERTEX_POINT ( 'NONE', #32355 ) ;
#9048=CIRCLE ( 'NONE', #6175, 17.49900000000001654 ) ;
#9064=CARTESIAN_POINT ( 'NONE',  ( 8.000000000000000000, -9.471478019455027209, -14.71414642875966017 ) ) ;
#9081=VERTEX_POINT ( 'NONE', #10572 ) ;
#9090=FACE_OUTER_BOUND ( 'NONE', #5688, .T. ) ;
#9117=ORIENTED_EDGE ( 'NONE', *, *, #34427, .T. ) ;
#9119=DIRECTION ( 'NONE',  ( 0.000000000000000000, 0.000000000000000000, -1.000000000000000000 ) ) ;
#9136=DIRECTION ( 'NONE',  ( -1.000000000000000000, 0.000000000000000000, 0.000000000000000000 ) ) ;
#9158=CARTESIAN_POINT ( 'NONE',  ( 8.000000000000000000, 4.460989585140964664, 16.92083251265327348 ) ) ;
#9187=FACE_OUTER_BOUND ( 'NONE', #2718, .T. ) ;
#9217=ORIENTED_EDGE ( 'NONE', *, *, #21129, .T. ) ;
#9218=ORIENTED_EDGE ( 'NONE', *, *, #30407, .T. ) ;
#9235=FACE_OUTER_BOUND ( 'NONE', #26695, .T. ) ;
#9249=CARTESIAN_POINT ( 'NONE',  ( 0.000000000000000000, 0.000000000000000000, 0.000000000000000000 ) ) ;
#9261=ORIENTED_EDGE ( 'NONE', *, *, #14136, .F. ) ;
#9270=DIRECTION ( 'NONE',  ( 0.000000000000000000, 0.000000000000000000, 1.000000000000000000 ) ) ;
#9277=VERTEX_POINT ( 'NONE', #34669 ) ;
#9288=DIRECTION ( 'NONE',  ( -1.000000000000000000, 0.000000000000000000, 0.000000000000000000 ) ) ;
#9304=VERTEX_POINT ( 'NONE', #11233 ) ;
#9313=DIRECTION ( 'NONE',  ( 0.000000000000000000, -6.938893903907228378E-15, 1.000000000000000000 ) ) ;
#9317=FACE_OUTER_BOUND ( 'NONE', #23780, .T. ) ;
#9329=CARTESIAN_POINT ( 'NONE',  ( 8.000000000000000000, 16.53603053422211389, 8.931325931664652273 ) ) ;
#9332=ORIENTED_EDGE ( 'NONE', *, *, #4442, .F. ) ;
#9357=VECTOR ( 'NONE', #21095, 1000.000000000000000 ) ;
#9369=EDGE_CURVE ( 'NONE', #17571, #5963, #29621, .T. ) ;
#9370=EDGE_LOOP ( 'NONE', ( #1368, #11901, #27951, #13082 ) ) ;
#9397=ORIENTED_EDGE ( 'NONE', *, *, #10411, .F. ) ;
#9400=AXIS2_PLACEMENT_3D ( 'NONE', #15418, #23904, #4120 ) ;
#9406=DIRECTION ( 'NONE',  ( 0.000000000000000000, 1.000000000000000000, 3.491564676272318479E-15 ) ) ;
#9410=AXIS2_PLACEMENT_3D ( 'NONE', #29077, #10170, #1533 ) ;
#9411=DIRECTION ( 'NONE',  ( -1.000000000000000000, 0.000000000000000000, 0.000000000000000000 ) ) ;
#9413=CARTESIAN_POINT ( 'NONE',  ( 8.000000000000000000, 0.000000000000000000, 0.000000000000000000 ) ) ;
#9432=ORIENTED_EDGE ( 'NONE', *, *, #3164, .T. ) ;
#9433=ORIENTED_EDGE ( 'NONE', *, *, #13879, .F. ) ;
#9503=CYLINDRICAL_SURFACE ( 'NONE', #20135, 17.49900000000000233 ) ;
#9514=ORIENTED_EDGE ( 'NONE', *, *, #21129, .F. ) ;
#9518=CARTESIAN_POINT ( 'NONE',  ( 8.000000000000000000, -13.55483219355720337, -11.06713717293254362 ) ) ;
#9535=CARTESIAN_POINT ( 'NONE',  ( 8.000000000000000000, -11.06713717293229138, -13.55483219355740765 ) ) ;
#9536=VERTEX_POINT ( 'NONE', #5835 ) ;
#9540=CYLINDRICAL_SURFACE ( 'NONE', #29815, 22.00000000000000000 ) ;
#9549=AXIS2_PLACEMENT_3D ( 'NONE', #12000, #10003, #18280 ) ;
#9552=EDGE_LOOP ( 'NONE', ( #26997, #3261, #21069, #6931 ) ) ;
#9584=EDGE_LOOP ( 'NONE', ( #18939, #501, #8942, #16858 ) ) ;
#9589=CARTESIAN_POINT ( 'NONE',  ( 8.000000000000000000, -6.336799421339930127, 16.31134495048480915 ) ) ;
#9592=AXIS2_PLACEMENT_3D ( 'NONE', #30756, #3411, #33624 ) ;
#9604=CARTESIAN_POINT ( 'NONE',  ( 0.000000000000000000, -16.94522934049206597, -8.128228055639052485 ) ) ;
#9629=VECTOR ( 'NONE', #17200, 1000.000000000000000 ) ;
#9635=UNCERTAINTY_MEASURE_WITH_UNIT (LENGTH_MEASURE( 1.000000000000000082E-05 ), #19540, 'distance_accuracy_value', 'NONE');
#9636=CARTESIAN_POINT ( 'NONE',  ( 0.000000000000000000, 16.31134495048493704, -6.336799421339641469 ) ) ;
#9654=ORIENTED_EDGE ( 'NONE', *, *, #28275, .F. ) ;
#9658=VERTEX_POINT ( 'NONE', #14275 ) ;
#9675=DIRECTION ( 'NONE',  ( -1.000000000000000000, 0.000000000000000000, 0.000000000000000000 ) ) ;
#9692=ADVANCED_FACE ( 'NONE', ( #7242 ), #28691, .T. ) ;
#9699=ORIENTED_EDGE ( 'NONE', *, *, #6816, .F. ) ;
#9717=ADVANCED_FACE ( 'NONE', ( #6710 ), #12295, .T. ) ;
#9727=LINE ( 'NONE', #20517, #30227 ) ;
#9732=CARTESIAN_POINT ( 'NONE',  ( 50.00005079999999680, 5.400000000000021672, 1.000000000000001776 ) ) ;
#9733=EDGE_CURVE ( 'NONE', #34692, #15039, #1864, .T. ) ;
#9752=CARTESIAN_POINT ( 'NONE',  ( 8.000000000000000000, 2.912696353506122104, -21.80633394113446855 ) ) ;
#9760=VERTEX_POINT ( 'NONE', #4750 ) ;
#9777=AXIS2_PLACEMENT_3D ( 'NONE', #32705, #29298, #4648 ) ;
#9782=CARTESIAN_POINT ( 'NONE',  ( 0.000000000000000000, 2.494040418455352182, 18.62763138773848937 ) ) ;
#9786=CARTESIAN_POINT ( 'NONE',  ( 0.000000000000000000, 0.000000000000000000, 0.000000000000000000 ) ) ;
#9790=ORIENTED_EDGE ( 'NONE', *, *, #9733, .F. ) ;
#9801=DIRECTION ( 'NONE',  ( 0.000000000000000000, 0.5877852522924739143, -0.8090169943749470072 ) ) ;
#9829=ORIENTED_EDGE ( 'NONE', *, *, #23855, .T. ) ;
#9838=EDGE_LOOP ( 'NONE', ( #19907, #9860, #14024, #16815 ) ) ;
#9851=CARTESIAN_POINT ( 'NONE',  ( 8.000000000000000000, -3.384281271887680909, -18.48663108841362757 ) ) ;
#9854=CARTESIAN_POINT ( 'NONE',  ( 50.00005079999999680, 0.000000000000000000, 0.000000000000000000 ) ) ;
#9860=ORIENTED_EDGE ( 'NONE', *, *, #32433, .T. ) ;
#9867=DIRECTION ( 'NONE',  ( 1.000000000000000000, -0.000000000000000000, 0.000000000000000000 ) ) ;
#9888=CARTESIAN_POINT ( 'NONE',  ( 8.000000000000000000, -0.9861715913086367413, -17.47118961583605312 ) ) ;
#9892=FACE_OUTER_BOUND ( 'NONE', #11508, .T. ) ;
#9894=DIRECTION ( 'NONE',  ( -1.000000000000000000, 0.000000000000000000, 0.000000000000000000 ) ) ;
#9898=ADVANCED_FACE ( 'NONE', ( #24006 ), #35343, .T. ) ;
#9904=EDGE_CURVE ( 'NONE', #16930, #7329, #19108, .T. ) ;
#9906=AXIS2_PLACEMENT_3D ( 'NONE', #13611, #33399, #16651 ) ;
#9923=ORIENTED_EDGE ( 'NONE', *, *, #13107, .T. ) ;
#9924=DIRECTION ( 'NONE',  ( -1.000000000000000000, 0.000000000000000000, 0.000000000000000000 ) ) ;
#9926=ORIENTED_EDGE ( 'NONE', *, *, #19957, .T. ) ;
#9942=DIRECTION ( 'NONE',  ( -1.000000000000000000, 0.000000000000000000, 0.000000000000000000 ) ) ;
#9950=CARTESIAN_POINT ( 'NONE',  ( 8.000000000000000000, 2.912696353505818792, 21.80633394113451118 ) ) ;
#9952=ORIENTED_EDGE ( 'NONE', *, *, #15490, .T. ) ;
#9954=AXIS2_PLACEMENT_3D ( 'NONE', #23464, #28504, #15156 ) ;
#9964=DIRECTION ( 'NONE',  ( -1.000000000000000000, 0.000000000000000000, 0.000000000000000000 ) ) ;
#9968=ORIENTED_EDGE ( 'NONE', *, *, #34122, .F. ) ;
#9979=VECTOR ( 'NONE', #5244, 1000.000000000000000 ) ;
#10003=DIRECTION ( 'NONE',  ( 1.000000000000000000, -0.000000000000000000, 0.000000000000000000 ) ) ;
#10018=EDGE_CURVE ( 'NONE', #34251, #14155, #30984, .T. ) ;
#10082=DIRECTION ( 'NONE',  ( 0.000000000000000000, 0.3090169943749412895, 0.9510565162951555296 ) ) ;
#10096=CIRCLE ( 'NONE', #14677, 8.000000000000007105 ) ;
#10101=DIRECTION ( 'NONE',  ( 0.000000000000000000, -0.5877852522924796874, 0.8090169943749426773 ) ) ;
#10110=LINE ( 'NONE', #15139, #8154 ) ;
#10111=ORIENTED_EDGE ( 'NONE', *, *, #16990, .T. ) ;
#10114=CIRCLE ( 'NONE', #26229, 22.00000000000000000 ) ;
#10125=FACE_OUTER_BOUND ( 'NONE', #4817, .T. ) ;
#10128=CARTESIAN_POINT ( 'NONE',  ( 8.000000000000000000, 0.000000000000000000, 0.000000000000000000 ) ) ;
#10135=DIRECTION ( 'NONE',  ( -1.000000000000000000, 0.000000000000000000, 0.000000000000000000 ) ) ;
#10143=FACE_OUTER_BOUND ( 'NONE', #19519, .T. ) ;
#10170=DIRECTION ( 'NONE',  ( -1.000000000000000000, 0.000000000000000000, 0.000000000000000000 ) ) ;
#10177=DIRECTION ( 'NONE',  ( 0.000000000000000000, 0.000000000000000000, -1.000000000000000000 ) ) ;
#10188=ADVANCED_FACE ( 'NONE', ( #21368 ), #10231, .T. ) ;
#10190=AXIS2_PLACEMENT_3D ( 'NONE', #33288, #25004, #8604 ) ;
#10195=DIRECTION ( 'NONE',  ( -1.000000000000000000, 0.000000000000000000, 0.000000000000000000 ) ) ;
#10210=ORIENTED_EDGE ( 'NONE', *, *, #23855, .F. ) ;
#10217=CARTESIAN_POINT ( 'NONE',  ( 8.000000000000000000, 0.000000000000000000, 0.000000000000000000 ) ) ;
#10224=AXIS2_PLACEMENT_3D ( 'NONE', #20990, #26424, #1755 ) ;
#10231=CYLINDRICAL_SURFACE ( 'NONE', #31009, 8.000000000000003553 ) ;
#10236=DIRECTION ( 'NONE',  ( 0.000000000000000000, 0.5877852522924682521, 0.8090169943749511150 ) ) ;
#10250=VECTOR ( 'NONE', #14654, 1000.000000000000000 ) ;
#10265=DIRECTION ( 'NONE',  ( -1.000000000000000000, 0.000000000000000000, 0.000000000000000000 ) ) ;
#10275=ORIENTED_EDGE ( 'NONE', *, *, #16140, .T. ) ;
#10284=ORIENTED_EDGE ( 'NONE', *, *, #5523, .F. ) ;
#10302=ORIENTED_EDGE ( 'NONE', *, *, #24516, .T. ) ;
#10325=DIRECTION ( 'NONE',  ( -1.000000000000000000, 0.000000000000000000, 0.000000000000000000 ) ) ;
#10331=ORIENTED_EDGE ( 'NONE', *, *, #2711, .F. ) ;
#10336=SHAPE_REPRESENTATION_RELATIONSHIP ( 'NONE' , 'NONE' ,  #8186, #16793 ) ;
#10337=CARTESIAN_POINT ( 'NONE',  ( 0.000000000000000000, 0.000000000000000000, 0.000000000000000000 ) ) ;
#10350=CYLINDRICAL_SURFACE ( 'NONE', #31838, 8.000000000000001776 ) ;
#10359=DIRECTION ( 'NONE',  ( -1.000000000000000000, 0.000000000000000000, 0.000000000000000000 ) ) ;
#10363=CARTESIAN_POINT ( 'NONE',  ( 0.000000000000000000, 0.000000000000000000, 0.000000000000000000 ) ) ;
#10368=ADVANCED_FACE ( 'NONE', ( #27509 ), #3020, .T. ) ;
#10370=MANIFOLD_SOLID_BREP ( 'Keyway', #4341 ) ;
#10374=DIRECTION ( 'NONE',  ( 0.000000000000000000, 0.000000000000000000, 1.000000000000000000 ) ) ;
#10397=CYLINDRICAL_SURFACE ( 'NONE', #26621, 8.000000000000001776 ) ;
#10408=DIRECTION ( 'NONE',  ( -1.000000000000000000, 0.000000000000000000, 0.000000000000000000 ) ) ;
#10411=EDGE_CURVE ( 'NONE', #4187, #21532, #11996, .T. ) ;
#10433=DIRECTION ( 'NONE',  ( 0.000000000000000000, 0.000000000000000000, 1.000000000000000000 ) ) ;
#10447=CARTESIAN_POINT ( 'NONE',  ( 8.000000000000000000, 6.336799421339808447, 16.31134495048485533 ) ) ;
#10468=ORIENTED_EDGE ( 'NONE', *, *, #17976, .F. ) ;
#10513=CIRCLE ( 'NONE', #32926, 22.00000000000000000 ) ;
#10514=AXIS2_PLACEMENT_3D ( 'NONE', #26024, #17900, #18439 ) ;
#10518=DIRECTION ( 'NONE',  ( -1.000000000000000000, 0.000000000000000000, 0.000000000000000000 ) ) ;
#10523=LINE ( 'NONE', #15911, #31263 ) ;
#10542=AXIS2_PLACEMENT_3D ( 'NONE', #21668, #26742, #22028 ) ;
#10543=CARTESIAN_POINT ( 'NONE',  ( 4.000000000000003553, -19.83898331853678343, -9.508666619816859011 ) ) ;
#10546=CARTESIAN_POINT ( 'NONE',  ( 8.000000000000000000, 0.000000000000000000, -1.000000000000000222 ) ) ;
#10560=ADVANCED_FACE ( 'NONE', ( #4623 ), #15380, .T. ) ;
#10572=CARTESIAN_POINT ( 'NONE',  ( 0.000000000000000000, 18.48663108841359559, 4.615718728112120139 ) ) ;
#10591=ORIENTED_EDGE ( 'NONE', *, *, #21601, .F. ) ;
#10599=EDGE_LOOP ( 'NONE', ( #27398, #17362, #3068, #14836 ) ) ;
#10630=ORIENTED_EDGE ( 'NONE', *, *, #6603, .T. ) ;
#10633=CIRCLE ( 'NONE', #29608, 8.000000000000014211 ) ;
#10634=CARTESIAN_POINT ( 'NONE',  ( 8.000000000000000000, 9.471478019455140895, 14.71414642875960332 ) ) ;
#10675=DIRECTION ( 'NONE',  ( -1.000000000000000000, 0.000000000000000000, 0.000000000000000000 ) ) ;
#10682=CIRCLE ( 'NONE', #32513, 17.49900000000001299 ) ;
#10697=DIRECTION ( 'NONE',  ( 1.000000000000000000, -0.000000000000000000, 0.000000000000000000 ) ) ;
#10718=LINE ( 'NONE', #35580, #8994 ) ;
#10757=DIRECTION ( 'NONE',  ( -1.000000000000000000, 0.000000000000000000, 0.000000000000000000 ) ) ;
#10777=FACE_OUTER_BOUND ( 'NONE', #13164, .T. ) ;
#10778=EDGE_CURVE ( 'NONE', #16643, #32151, #24761, .T. ) ;
#10799=CIRCLE ( 'NONE', #15364, 8.000000000000015987 ) ;
#10815=EDGE_CURVE ( 'NONE', #15158, #27081, #16683, .T. ) ;
#10816=DIRECTION ( 'NONE',  ( 0.000000000000000000, 0.000000000000000000, -1.000000000000000000 ) ) ;
#10818=EDGE_CURVE ( 'NONE', #24162, #12885, #5781, .T. ) ;
#10819=VECTOR ( 'NONE', #20854, 1000.000000000000000 ) ;
#10841=DIRECTION ( 'NONE',  ( -1.000000000000000000, 0.000000000000000000, 0.000000000000000000 ) ) ;
#10844=EDGE_CURVE ( 'NONE', #25690, #11512, #18813, .T. ) ;
#10863=CARTESIAN_POINT ( 'NONE',  ( 0.000000000000000000, 6.336799421340039373, -16.31134495048478428 ) ) ;
#10873=ORIENTED_EDGE ( 'NONE', *, *, #14483, .F. ) ;
#10910=CARTESIAN_POINT ( 'NONE',  ( 8.000000000000000000, 19.83898331853685448, 9.508666619816709797 ) ) ;
#10918=CYLINDRICAL_SURFACE ( 'NONE', #15616, 8.000000000000001776 ) ;
#10923=AXIS2_PLACEMENT_3D ( 'NONE', #26575, #29631, #2283 ) ;
#10928=DIRECTION ( 'NONE',  ( 1.000000000000000000, -0.000000000000000000, 0.000000000000000000 ) ) ;
#10938=ORIENTED_EDGE ( 'NONE', *, *, #21207, .F. ) ;
#10948=EDGE_LOOP ( 'NONE', ( #35273, #16777, #2360, #26444 ) ) ;
#10951=AXIS2_PLACEMENT_3D ( 'NONE', #8800, #3248, #33473 ) ;
#10956=CARTESIAN_POINT ( 'NONE',  ( 4.000000000000003553, 15.92965478239619515, 15.17386234660388844 ) ) ;
#10974=CYLINDRICAL_SURFACE ( 'NONE', #10190, 8.000000000000000000 ) ;
#11036=EDGE_LOOP ( 'NONE', ( #29463, #9968, #227, #15399 ) ) ;
#11043=DIRECTION ( 'NONE',  ( 0.000000000000000000, -0.3090169943749350723, -0.9510565162951576390 ) ) ;
#11049=VECTOR ( 'NONE', #277, 1000.000000000000000 ) ;
#11050=CARTESIAN_POINT ( 'NONE',  ( 8.000000000000000000, 18.62763138773855687, 10.49404041845541968 ) ) ;
#11061=CARTESIAN_POINT ( 'NONE',  ( 8.000000000000000000, -18.62763138773852134, 2.494040418455287345 ) ) ;
#11098=CARTESIAN_POINT ( 'NONE',  ( 0.000000000000000000, 3.872983346207416133, -1.000000000000000000 ) ) ;
#11118=ORIENTED_EDGE ( 'NONE', *, *, #831, .F. ) ;
#11123=DIRECTION ( 'NONE',  ( 0.000000000000000000, 0.000000000000000000, 1.000000000000000000 ) ) ;
#11143=CIRCLE ( 'NONE', #23212, 8.000000000000001776 ) ;
#11185=CARTESIAN_POINT ( 'NONE',  ( 0.000000000000000000, 2.494040418455619523, -18.62763138773847871 ) ) ;
#11187=AXIS2_PLACEMENT_3D ( 'NONE', #1734, #10195, #26950 ) ;
#11194=VERTEX_POINT ( 'NONE', #24015 ) ;
#11206=ORIENTED_EDGE ( 'NONE', *, *, #28162, .T. ) ;
#11207=EDGE_CURVE ( 'NONE', #34510, #13434, #14981, .T. ) ;
#11214=CIRCLE ( 'NONE', #31336, 17.49900000000002720 ) ;
#11222=AXIS2_PLACEMENT_3D ( 'NONE', #6249, #28575, #22797 ) ;
#11229=FACE_OUTER_BOUND ( 'NONE', #13858, .T. ) ;
#11233=CARTESIAN_POINT ( 'NONE',  ( 0.000000000000000000, 3.872983346207429900, 1.000000000000003109 ) ) ;
#11239=CARTESIAN_POINT ( 'NONE',  ( 8.000000000000000000, -16.94522934049206597, -8.128228055639052485 ) ) ;
#11245=AXIS2_PLACEMENT_3D ( 'NONE', #32687, #21868, #2453 ) ;
#11265=DIRECTION ( 'NONE',  ( -1.000000000000000000, 0.000000000000000000, 0.000000000000000000 ) ) ;
#11311=DIRECTION ( 'NONE',  ( -1.000000000000000000, 0.000000000000000000, 0.000000000000000000 ) ) ;
#11320=CARTESIAN_POINT ( 'NONE',  ( 0.000000000000000000, 0.000000000000000000, 0.000000000000000000 ) ) ;
#11324=EDGE_CURVE ( 'NONE', #24581, #21764, #2382, .T. ) ;
#11344=ORIENTED_EDGE ( 'NONE', *, *, #11976, .T. ) ;
#11389=CARTESIAN_POINT ( 'NONE',  ( 8.000000000000000000, 11.06713717293239441, 13.55483219355733837 ) ) ;
#11390=EDGE_LOOP ( 'NONE', ( #28709, #11599, #22835, #7730 ) ) ;
#11393=ORIENTED_EDGE ( 'NONE', *, *, #32404, .T. ) ;
#11417=ORIENTED_EDGE ( 'NONE', *, *, #16911, .F. ) ;
#11422=VECTOR ( 'NONE', #16468, 1000.000000000000000 ) ;
#11428=CARTESIAN_POINT ( 'NONE',  ( 4.000000000000003553, 19.83898331853701080, -9.508666619816445120 ) ) ;
#11443=CYLINDRICAL_SURFACE ( 'NONE', #29816, 8.000000000000000000 ) ;
#11461=DIRECTION ( 'NONE',  ( 0.000000000000000000, 0.000000000000000000, 1.000000000000000000 ) ) ;
#11462=CARTESIAN_POINT ( 'NONE',  ( 8.000000000000000000, 3.968388925834817282, 21.63912866391138934 ) ) ;
#11464=ORIENTED_EDGE ( 'NONE', *, *, #6859, .F. ) ;
#11467=DIRECTION ( 'NONE',  ( 0.000000000000000000, 0.5877852522924739143, -0.8090169943749468962 ) ) ;
#11468=ORIENTED_EDGE ( 'NONE', *, *, #26688, .T. ) ;
#11470=ORIENTED_EDGE ( 'NONE', *, *, #14972, .F. ) ;
#11474=EDGE_CURVE ( 'NONE', #15158, #26182, #739, .T. ) ;
#11481=EDGE_CURVE ( 'NONE', #3480, #4713, #11720, .T. ) ;
#11501=EDGE_LOOP ( 'NONE', ( #35233, #28614, #9117, #32742 ) ) ;
#11508=EDGE_LOOP ( 'NONE', ( #12940, #13852, #10331, #34160 ) ) ;
#11512=VERTEX_POINT ( 'NONE', #23425 ) ;
#11571=ORIENTED_EDGE ( 'NONE', *, *, #25168, .F. ) ;
#11582=DIRECTION ( 'NONE',  ( -1.000000000000000000, 0.000000000000000000, 0.000000000000000000 ) ) ;
#11584=DIRECTION ( 'NONE',  ( 0.000000000000000000, 8.881784197001252323E-16, 1.000000000000000000 ) ) ;
#11597=EDGE_LOOP ( 'NONE', ( #14798, #9790, #33308, #24364 ) ) ;
#11599=ORIENTED_EDGE ( 'NONE', *, *, #12102, .T. ) ;
#11605=EDGE_CURVE ( 'NONE', #9760, #3460, #34594, .T. ) ;
#11609=CARTESIAN_POINT ( 'NONE',  ( 8.000000000000000000, 0.000000000000000000, 0.000000000000000000 ) ) ;
#11614=DIRECTION ( 'NONE',  ( 0.000000000000000000, 0.3090169943749477288, -0.9510565162951534202 ) ) ;
#11616=CIRCLE ( 'NONE', #13363, 4.000000000000000000 ) ;
#11618=DIRECTION ( 'NONE',  ( 0.000000000000000000, 1.000000000000000000, 3.469446951953614189E-15 ) ) ;
#11631=ORIENTED_EDGE ( 'NONE', *, *, #19598, .F. ) ;
#11635=ORIENTED_EDGE ( 'NONE', *, *, #12466, .T. ) ;
#11655=CARTESIAN_POINT ( 'NONE',  ( -10.00000000000000178, 0.000000000000000000, 0.000000000000000000 ) ) ;
#11663=DIRECTION ( 'NONE',  ( 0.000000000000000000, 0.000000000000000000, 1.000000000000000000 ) ) ;
#11671=AXIS2_PLACEMENT_3D ( 'NONE', #614, #27293, #22221 ) ;
#11706=AXIS2_PLACEMENT_3D ( 'NONE', #34353, #7150, #28768 ) ;
#11720=LINE ( 'NONE', #14064, #23056 ) ;
#11723=ORIENTED_EDGE ( 'NONE', *, *, #18796, .T. ) ;
#11730=EDGE_CURVE ( 'NONE', #6546, #27973, #6085, .T. ) ;
#11732=EDGE_CURVE ( 'NONE', #17296, #21628, #12743, .T. ) ;
#11754=DIRECTION ( 'NONE',  ( -1.000000000000000000, 0.000000000000000000, 0.000000000000000000 ) ) ;
#11757=ORIENTED_EDGE ( 'NONE', *, *, #20929, .F. ) ;
#11797=CARTESIAN_POINT ( 'NONE',  ( 0.000000000000000000, -2.494040418455211849, -18.62763138773853200 ) ) ;
#11798=CARTESIAN_POINT ( 'NONE',  ( 8.000000000000000000, -3.968388925834658743, -21.63912866391144263 ) ) ;
#11824=CIRCLE ( 'NONE', #6077, 17.49900000000001654 ) ;
#11827=ORIENTED_EDGE ( 'NONE', *, *, #22973, .T. ) ;
#11828=LINE ( 'NONE', #22808, #2740 ) ;
#11839=CARTESIAN_POINT ( 'NONE',  ( 0.000000000000000000, -21.80633394113452539, 2.912696353505745517 ) ) ;
#11847=EDGE_LOOP ( 'NONE', ( #5929, #26121, #31442, #23776 ) ) ;
#11859=EDGE_CURVE ( 'NONE', #6495, #27914, #30930, .T. ) ;
#11860=VERTEX_POINT ( 'NONE', #34442 ) ;
#11861=CIRCLE ( 'NONE', #14701, 17.49900000000000233 ) ;
#11894=ORIENTED_EDGE ( 'NONE', *, *, #29552, .T. ) ;
#11900=DIRECTION ( 'NONE',  ( -1.000000000000000000, 0.000000000000000000, 0.000000000000000000 ) ) ;
#11901=ORIENTED_EDGE ( 'NONE', *, *, #1502, .F. ) ;
#11918=CARTESIAN_POINT ( 'NONE',  ( 8.000000000000000000, 18.48663108841359559, 4.615718728112120139 ) ) ;
#11928=DIRECTION ( 'NONE',  ( 1.000000000000000000, -0.000000000000000000, 0.000000000000000000 ) ) ;
#11945=CARTESIAN_POINT ( 'NONE',  ( 8.000000000000000000, 0.000000000000000000, 0.000000000000000000 ) ) ;
#11946=EDGE_CURVE ( 'NONE', #23114, #9009, #10110, .T. ) ;
#11951=CARTESIAN_POINT ( 'NONE',  ( 8.000000000000000000, 4.460989585141205360, -16.92083251265323085 ) ) ;
#11957=EDGE_CURVE ( 'NONE', #14072, #1616, #29427, .T. ) ;
#11959=VERTEX_POINT ( 'NONE', #18387 ) ;
#11968=ORIENTED_EDGE ( 'NONE', *, *, #2986, .F. ) ;
#11970=CARTESIAN_POINT ( 'NONE',  ( 8.000000000000000000, 10.46102064772339979, 19.35373470438986487 ) ) ;
#11976=EDGE_CURVE ( 'NONE', #1074, #34100, #13893, .T. ) ;
#11996=LINE ( 'NONE', #6056, #31621 ) ;
#12000=CARTESIAN_POINT ( 'NONE',  ( 0.000000000000000000, -13.60411018104326963, 12.96676809804144348 ) ) ;
#12007=ORIENTED_EDGE ( 'NONE', *, *, #24199, .F. ) ;
#12009=DIRECTION ( 'NONE',  ( -1.000000000000000000, 0.000000000000000000, 0.000000000000000000 ) ) ;
#12014=CIRCLE ( 'NONE', #14856, 22.00000000000000000 ) ;
#12022=CARTESIAN_POINT ( 'NONE',  ( 0.000000000000000000, -19.35373470438975119, -10.46102064772362183 ) ) ;
#12024=CARTESIAN_POINT ( 'NONE',  ( 0.000000000000000000, 0.000000000000000000, 0.000000000000000000 ) ) ;
#12049=FACE_OUTER_BOUND ( 'NONE', #20126, .T. ) ;
#12050=ORIENTED_EDGE ( 'NONE', *, *, #19171, .T. ) ;
#12060=DIRECTION ( 'NONE',  ( 0.000000000000000000, 0.9510565162951545304, -0.3090169943749448977 ) ) ;
#12063=CYLINDRICAL_SURFACE ( 'NONE', #14952, 8.000000000000001776 ) ;
#12068=CARTESIAN_POINT ( 'NONE',  ( 8.000000000000000000, 18.62763138773855687, 2.494040418455418351 ) ) ;
#12102=EDGE_CURVE ( 'NONE', #23663, #28798, #27705, .T. ) ;
#12130=EDGE_LOOP ( 'NONE', ( #3026, #15043, #21222, #19499 ) ) ;
#12155=DIRECTION ( 'NONE',  ( 0.000000000000000000, 0.5877852522924681411, 0.8090169943749510040 ) ) ;
#12156=CARTESIAN_POINT ( 'NONE',  ( 4.000000000000003553, -21.80633394113448276, -2.912696353506054159 ) ) ;
#12163=DIRECTION ( 'NONE',  ( 0.000000000000000000, 0.000000000000000000, 1.000000000000000000 ) ) ;
#12167=ORIENTED_EDGE ( 'NONE', *, *, #16956, .F. ) ;
#12172=CARTESIAN_POINT ( 'NONE',  ( 8.000000000000000000, 12.96676809804168862, -13.60411018104304048 ) ) ;
#12175=VERTEX_POINT ( 'NONE', #25527 ) ;
#12176=VERTEX_POINT ( 'NONE', #843 ) ;
#12202=DIRECTION ( 'NONE',  ( -1.000000000000000000, 0.000000000000000000, 0.000000000000000000 ) ) ;
#12221=EDGE_CURVE ( 'NONE', #32738, #14850, #20095, .T. ) ;
#12251=DIRECTION ( 'NONE',  ( -1.000000000000000000, 0.000000000000000000, 0.000000000000000000 ) ) ;
#12262=CIRCLE ( 'NONE', #17404, 17.49900000000001299 ) ;
#12263=EDGE_CURVE ( 'NONE', #35453, #12842, #15053, .T. ) ;
#12270=CIRCLE ( 'NONE', #15123, 8.000000000000010658 ) ;
#12283=ORIENTED_EDGE ( 'NONE', *, *, #4352, .T. ) ;
#12286=AXIS2_PLACEMENT_3D ( 'NONE', #11061, #27456, #35077 ) ;
#12294=VECTOR ( 'NONE', #35419, 1000.000000000000000 ) ;
#12295=CYLINDRICAL_SURFACE ( 'NONE', #3929, 17.49900000000000233 ) ;
#12298=ORIENTED_EDGE ( 'NONE', *, *, #20257, .T. ) ;
#12312=ORIENTED_EDGE ( 'NONE', *, *, #25817, .F. ) ;
#12316=EDGE_CURVE ( 'NONE', #26583, #24162, #4171, .T. ) ;
#12322=CARTESIAN_POINT ( 'NONE',  ( 8.000000000000000000, -17.47118961583598917, -0.9861715913089493801 ) ) ;
#12338=CIRCLE ( 'NONE', #15196, 8.000000000000008882 ) ;
#12345=ADVANCED_FACE ( 'NONE', ( #35071, #7668 ), #18477, .F. ) ;
#12356=ORIENTED_EDGE ( 'NONE', *, *, #19965, .T. ) ;
#12357=EDGE_CURVE ( 'NONE', #25593, #4447, #24086, .T. ) ;
#12382=DIRECTION ( 'NONE',  ( 0.000000000000000000, 0.000000000000000000, 1.000000000000000000 ) ) ;
#12388=EDGE_CURVE ( 'NONE', #16691, #29018, #32916, .T. ) ;
#12397=AXIS2_PLACEMENT_3D ( 'NONE', #30511, #22041, #16451 ) ;
#12409=ORIENTED_EDGE ( 'NONE', *, *, #23489, .T. ) ;
#12434=VERTEX_POINT ( 'NONE', #18299 ) ;
#12452=AXIS2_PLACEMENT_3D ( 'NONE', #35426, #10757, #8738 ) ;
#12466=EDGE_CURVE ( 'NONE', #27894, #3460, #32785, .T. ) ;
#12488=CARTESIAN_POINT ( 'NONE',  ( 8.000000000000000000, 0.000000000000000000, 0.000000000000000000 ) ) ;
#12501=AXIS2_PLACEMENT_3D ( 'NONE', #12738, #29484, #20632 ) ;
#12504=CIRCLE ( 'NONE', #22845, 8.000000000000007105 ) ;
#12507=EDGE_CURVE ( 'NONE', #4187, #4766, #18976, .T. ) ;
#12509=CARTESIAN_POINT ( 'NONE',  ( 8.000000000000000000, 8.128228055638880178, 16.94522934049213347 ) ) ;
#12516=ORIENTED_EDGE ( 'NONE', *, *, #1409, .F. ) ;
#12524=FACE_OUTER_BOUND ( 'NONE', #20120, .T. ) ;
#12530=AXIS2_PLACEMENT_3D ( 'NONE', #31855, #28809, #18352 ) ;
#12536=ORIENTED_EDGE ( 'NONE', *, *, #7507, .F. ) ;
#12561=CIRCLE ( 'NONE', #15414, 22.00000000000000000 ) ;
#12572=CYLINDRICAL_SURFACE ( 'NONE', #26150, 4.000000000000000000 ) ;
#12583=EDGE_LOOP ( 'NONE', ( #33053, #27784, #14832, #5589 ) ) ;
#12601=CARTESIAN_POINT ( 'NONE',  ( 8.000000000000000000, -17.47118961583602470, 0.9861715913087032437 ) ) ;
#12602=VERTEX_POINT ( 'NONE', #15283 ) ;
#12632=EDGE_CURVE ( 'NONE', #8203, #5984, #24132, .T. ) ;
#12640=CARTESIAN_POINT ( 'NONE',  ( 8.000000000000000000, 15.92965478239619515, 15.17386234660388666 ) ) ;
#12647=DIRECTION ( 'NONE',  ( -1.000000000000000000, 0.000000000000000000, 0.000000000000000000 ) ) ;
#12656=FACE_OUTER_BOUND ( 'NONE', #17600, .T. ) ;
#12671=FACE_OUTER_BOUND ( 'NONE', #4934, .T. ) ;
#12692=DIRECTION ( 'NONE',  ( 1.000000000000000000, -0.000000000000000000, -0.000000000000000000 ) ) ;
#12713=FACE_OUTER_BOUND ( 'NONE', #22053, .T. ) ;
#12725=DIRECTION ( 'NONE',  ( 0.000000000000000000, 0.000000000000000000, 1.000000000000000000 ) ) ;
#12729=CARTESIAN_POINT ( 'NONE',  ( 8.000000000000000000, -8.931325931664709117, 16.53603053422203573 ) ) ;
#12733=ORIENTED_EDGE ( 'NONE', *, *, #20910, .F. ) ;
#12738=CARTESIAN_POINT ( 'NONE',  ( -10.00000000000000178, 0.000000000000000000, 0.000000000000000000 ) ) ;
#12743=CIRCLE ( 'NONE', #32871, 17.49900000000001299 ) ;
#12766=EDGE_CURVE ( 'NONE', #20884, #6031, #30501, .T. ) ;
#12770=ADVANCED_FACE ( 'NONE', ( #24657 ), #12063, .T. ) ;
#12771=CARTESIAN_POINT ( 'NONE',  ( 8.000000000000000000, -8.931325931664709117, 16.53603053422203573 ) ) ;
#12786=DIRECTION ( 'NONE',  ( -1.000000000000000000, 0.000000000000000000, 0.000000000000000000 ) ) ;
#12797=AXIS2_PLACEMENT_3D ( 'NONE', #1751, #20627, #28936 ) ;
#12813=DIRECTION ( 'NONE',  ( -1.000000000000000000, 0.000000000000000000, 0.000000000000000000 ) ) ;
#12816=CARTESIAN_POINT ( 'NONE',  ( 8.000000000000000000, -18.62763138773848581, -2.494040418455559127 ) ) ;
#12822=AXIS2_PLACEMENT_3D ( 'NONE', #6532, #14449, #25277 ) ;
#12842=VERTEX_POINT ( 'NONE', #11839 ) ;
#12844=AXIS2_PLACEMENT_3D ( 'NONE', #27598, #5629, #3459 ) ;
#12850=EDGE_CURVE ( 'NONE', #23114, #23381, #8608, .T. ) ;
#12853=ORIENTED_EDGE ( 'NONE', *, *, #16521, .F. ) ;
#12884=AXIS2_PLACEMENT_3D ( 'NONE', #16621, #11582, #19498 ) ;
#12885=VERTEX_POINT ( 'NONE', #3413 ) ;
#12888=DIRECTION ( 'NONE',  ( -1.000000000000000000, 0.000000000000000000, 0.000000000000000000 ) ) ;
#12896=CIRCLE ( 'NONE', #26705, 17.49900000000001299 ) ;
#12908=ORIENTED_EDGE ( 'NONE', *, *, #8672, .F. ) ;
#12909=ORIENTED_EDGE ( 'NONE', *, *, #15444, .T. ) ;
#12910=DIRECTION ( 'NONE',  ( 0.000000000000000000, 0.000000000000000000, 1.000000000000000000 ) ) ;
#12911=DIRECTION ( 'NONE',  ( -1.000000000000000000, 0.000000000000000000, 0.000000000000000000 ) ) ;
#12927=CARTESIAN_POINT ( 'NONE',  ( 8.000000000000000000, 0.000000000000000000, 0.000000000000000000 ) ) ;
#12930=ADVANCED_FACE ( 'NONE', ( #20462 ), #9503, .T. ) ;
#12940=ORIENTED_EDGE ( 'NONE', *, *, #7090, .T. ) ;
#12951=CIRCLE ( 'NONE', #13541, 8.000000000000007105 ) ;
#12954=ORIENTED_EDGE ( 'NONE', *, *, #31496, .T. ) ;
#12961=LINE ( 'NONE', #23946, #18301 ) ;
#12999=ORIENTED_EDGE ( 'NONE', *, *, #6859, .T. ) ;
#13005=AXIS2_PLACEMENT_3D ( 'NONE', #6100, #25015, #8788 ) ;
#13010=LINE ( 'NONE', #32797, #31185 ) ;
#13017=ORIENTED_EDGE ( 'NONE', *, *, #1789, .T. ) ;
#13051=CIRCLE ( 'NONE', #22228, 8.000000000000007105 ) ;
#13068=FACE_OUTER_BOUND ( 'NONE', #33882, .T. ) ;
#13082=ORIENTED_EDGE ( 'NONE', *, *, #24880, .T. ) ;
#13083=DIRECTION ( 'NONE',  ( -1.000000000000000000, 0.000000000000000000, 0.000000000000000000 ) ) ;
#13092=EDGE_CURVE ( 'NONE', #21954, #9760, #31639, .T. ) ;
#13096=DIRECTION ( 'NONE',  ( 1.000000000000000000, -0.000000000000000000, -0.000000000000000000 ) ) ;
#13107=EDGE_CURVE ( 'NONE', #23058, #16691, #26502, .T. ) ;
#13115=CARTESIAN_POINT ( 'NONE',  ( 0.000000000000000000, -9.508666619816507293, -19.83898331853700370 ) ) ;
#13117=DIRECTION ( 'NONE',  ( 0.000000000000000000, 0.000000000000000000, 1.000000000000000000 ) ) ;
#13127=CARTESIAN_POINT ( 'NONE',  ( 0.000000000000000000, -8.128228055638974325, 16.94522934049209795 ) ) ;
#13148=AXIS2_PLACEMENT_3D ( 'NONE', #22433, #3386, #24980 ) ;
#13156=LINE ( 'NONE', #20858, #14234 ) ;
#13164=EDGE_LOOP ( 'NONE', ( #21377, #25919, #18083, #15221 ) ) ;
#13176=ADVANCED_FACE ( 'NONE', ( #34901 ), #17948, .T. ) ;
#13197=CARTESIAN_POINT ( 'NONE',  ( 0.000000000000000000, 21.63912866391140710, 3.968388925834887893 ) ) ;
#13198=DIRECTION ( 'NONE',  ( -1.000000000000000000, 0.000000000000000000, 0.000000000000000000 ) ) ;
#13200=DIRECTION ( 'NONE',  ( -1.000000000000000000, 0.000000000000000000, 0.000000000000000000 ) ) ;
#13201=DIRECTION ( 'NONE',  ( -1.000000000000000000, 0.000000000000000000, 0.000000000000000000 ) ) ;
#13202=CARTESIAN_POINT ( 'NONE',  ( 8.000000000000000000, 16.31134495048485178, 6.336799421339877725 ) ) ;
#13204=EDGE_LOOP ( 'NONE', ( #32507, #17025, #8298, #32924, #3519, #17491, #940, #26468, #32033, #20159, #1554, #15945, #32700, #5989, #4629, #21832, #29940, #28483, #15743, #10468, #13708, #26327, #12007, #9654, #25052, #20721, #33590, #4727, #22453, #11470, #5206, #25517, #21744, #30163, #2104, #17503, #6259, #10591, #13547, #23638, #18816, #29289, #24398, #17619, #18951, #27134, #30553, #2348, #19973, #4313, #35069, #23152, #28873, #2995, #12733, #7022, #8540, #24118, #23422, #26866, #18783, #26308, #6209, #7654, #18105, #10284, #4753, #32411, #8494, #16941, #33930, #3126, #32331, #6147, #3974, #1507, #30957, #33532, #3564, #13596, #20804, #33600, #26236, #2912, #20531 ) ) ;
#13235=FACE_OUTER_BOUND ( 'NONE', #24770, .T. ) ;
#13249=CARTESIAN_POINT ( 'NONE',  ( 0.000000000000000000, -15.92965478239629817, 15.17386234660378008 ) ) ;
#13258=CARTESIAN_POINT ( 'NONE',  ( 0.000000000000000000, 0.000000000000000000, 0.000000000000000000 ) ) ;
#13278=CARTESIAN_POINT ( 'NONE',  ( 8.000000000000000000, 0.000000000000000000, 0.000000000000000000 ) ) ;
#13281=DIRECTION ( 'NONE',  ( 1.000000000000000000, -0.000000000000000000, 0.000000000000000000 ) ) ;
#13297=CARTESIAN_POINT ( 'NONE',  ( 8.000000000000000000, -15.17386234660395417, 15.92965478239613830 ) ) ;
#13316=CARTESIAN_POINT ( 'NONE',  ( 8.000000000000000000, 8.128228055638880178, 16.94522934049213347 ) ) ;
#13317=VECTOR ( 'NONE', #22520, 1000.000000000000000 ) ;
#13324=CARTESIAN_POINT ( 'NONE',  ( 0.000000000000000000, 8.128228055639098670, -16.94522934049206242 ) ) ;
#13327=EDGE_CURVE ( 'NONE', #9081, #21954, #8998, .T. ) ;
#13342=FACE_OUTER_BOUND ( 'NONE', #2023, .T. ) ;
#13343=AXIS2_PLACEMENT_3D ( 'NONE', #23447, #23987, #34980 ) ;
#13344=ORIENTED_EDGE ( 'NONE', *, *, #34549, .T. ) ;
#13358=ORIENTED_EDGE ( 'NONE', *, *, #17655, .T. ) ;
#13363=AXIS2_PLACEMENT_3D ( 'NONE', #30707, #27834, #14304 ) ;
#13396=DIRECTION ( 'NONE',  ( -1.000000000000000000, 0.000000000000000000, 0.000000000000000000 ) ) ;
#13403=CARTESIAN_POINT ( 'NONE',  ( 0.000000000000000000, 10.46102064772367868, -19.35373470438974053 ) ) ;
#13417=CARTESIAN_POINT ( 'NONE',  ( 4.000000000000003553, -10.46102064772354723, 19.35373470438981869 ) ) ;
#13419=CARTESIAN_POINT ( 'NONE',  ( 3.999999999999996447, 2.912696353506125657, -21.80633394113447210 ) ) ;
#13421=EDGE_CURVE ( 'NONE', #29017, #23042, #1532, .T. ) ;
#13423=CARTESIAN_POINT ( 'NONE',  ( 0.000000000000000000, 16.94522934049224361, -8.128228055638670568 ) ) ;
#13425=AXIS2_PLACEMENT_3D ( 'NONE', #16522, #8067, #2872 ) ;
#13428=DIRECTION ( 'NONE',  ( 0.000000000000000000, -6.983129352544636959E-15, 1.000000000000000000 ) ) ;
#13429=CYLINDRICAL_SURFACE ( 'NONE', #29771, 17.49900000000000233 ) ;
#13434=VERTEX_POINT ( 'NONE', #23136 ) ;
#13445=CARTESIAN_POINT ( 'NONE',  ( 8.000000000000000000, 0.000000000000000000, 0.000000000000000000 ) ) ;
#13448=DIRECTION ( 'NONE',  ( -1.000000000000000000, 0.000000000000000000, 0.000000000000000000 ) ) ;
#13472=ORIENTED_EDGE ( 'NONE', *, *, #11481, .T. ) ;
#13496=ADVANCED_FACE ( 'NONE', ( #3899 ), #14855, .T. ) ;
#13502=DIRECTION ( 'NONE',  ( 1.000000000000000000, -0.000000000000000000, 0.000000000000000000 ) ) ;
#13503=CARTESIAN_POINT ( 'NONE',  ( 50.00005079999999680, 5.399999999999999467, -1.000000000000003109 ) ) ;
#13510=ORIENTED_EDGE ( 'NONE', *, *, #11859, .F. ) ;
#13525=DIRECTION ( 'NONE',  ( -1.000000000000000000, 0.000000000000000000, 0.000000000000000000 ) ) ;
#13541=AXIS2_PLACEMENT_3D ( 'NONE', #27439, #5296, #11043 ) ;
#13547=ORIENTED_EDGE ( 'NONE', *, *, #12850, .F. ) ;
#13553=DIRECTION ( 'NONE',  ( -1.000000000000000000, 0.000000000000000000, 0.000000000000000000 ) ) ;
#13566=ORIENTED_EDGE ( 'NONE', *, *, #22127, .F. ) ;
#13570=DIRECTION ( 'NONE',  ( -1.000000000000000000, 0.000000000000000000, 0.000000000000000000 ) ) ;
#13577=CARTESIAN_POINT ( 'NONE',  ( 8.000000000000000000, -2.494040418455211849, -18.62763138773853200 ) ) ;
#13596=ORIENTED_EDGE ( 'NONE', *, *, #6207, .F. ) ;
#13606=CARTESIAN_POINT ( 'NONE',  ( 0.000000000000000000, 16.53603053422211389, 8.931325931664652273 ) ) ;
#13611=CARTESIAN_POINT ( 'NONE',  ( 0.000000000000000000, 0.000000000000000000, 0.000000000000000000 ) ) ;
#13613=AXIS2_PLACEMENT_3D ( 'NONE', #13423, #24404, #35391 ) ;
#13615=DIRECTION ( 'NONE',  ( -1.000000000000000000, 0.000000000000000000, 0.000000000000000000 ) ) ;
#13621=DIRECTION ( 'NONE',  ( 0.000000000000000000, -0.5877852522924799095, 0.8090169943749424553 ) ) ;
#13641=ORIENTED_EDGE ( 'NONE', *, *, #11605, .T. ) ;
#13642=ORIENTED_EDGE ( 'NONE', *, *, #20482, .T. ) ;
#13643=AXIS2_PLACEMENT_3D ( 'NONE', #21637, #16226, #18415 ) ;
#13654=ADVANCED_FACE ( 'NONE', ( #34672 ), #1361, .T. ) ;
#13664=EDGE_CURVE ( 'NONE', #7329, #23201, #6160, .T. ) ;
#13677=DIRECTION ( 'NONE',  ( 0.000000000000000000, 0.000000000000000000, 1.000000000000000000 ) ) ;
#13679=DIRECTION ( 'NONE',  ( -1.000000000000000000, 0.000000000000000000, 0.000000000000000000 ) ) ;
#13680=DIRECTION ( 'NONE',  ( -1.000000000000000000, 0.000000000000000000, 0.000000000000000000 ) ) ;
#13693=ORIENTED_EDGE ( 'NONE', *, *, #4611, .F. ) ;
#13698=CYLINDRICAL_SURFACE ( 'NONE', #8059, 8.000000000000001776 ) ;
#13707=FACE_OUTER_BOUND ( 'NONE', #15752, .T. ) ;
#13708=ORIENTED_EDGE ( 'NONE', *, *, #4605, .F. ) ;
#13717=CIRCLE ( 'NONE', #33835, 8.000000000000001776 ) ;
#13725=DIRECTION ( 'NONE',  ( 0.000000000000000000, 1.000000000000000000, 3.469446951953614189E-15 ) ) ;
#13744=ORIENTED_EDGE ( 'NONE', *, *, #24516, .F. ) ;
#13754=CARTESIAN_POINT ( 'NONE',  ( 8.000000000000000000, 0.000000000000000000, 0.000000000000000000 ) ) ;
#13758=DIRECTION ( 'NONE',  ( 0.000000000000000000, 0.000000000000000000, -1.000000000000000000 ) ) ;
#13780=LINE ( 'NONE', #22046, #364 ) ;
#13781=ORIENTED_EDGE ( 'NONE', *, *, #11207, .T. ) ;
#13782=CARTESIAN_POINT ( 'NONE',  ( 4.000000000000003553, 3.968388925835109049, -21.63912866391136447 ) ) ;
#13789=ORIENTED_EDGE ( 'NONE', *, *, #450, .T. ) ;
#13790=CARTESIAN_POINT ( 'NONE',  ( 8.000000000000000000, -2.494040418455483188, 18.62763138773849292 ) ) ;
#13793=CIRCLE ( 'NONE', #18385, 17.49900000000001299 ) ;
#13806=DIRECTION ( 'NONE',  ( 1.000000000000000000, -0.000000000000000000, -0.000000000000000000 ) ) ;
#13810=FILL_AREA_STYLE ('',( #122 ) ) ;
#13816=ORIENTED_EDGE ( 'NONE', *, *, #34093, .T. ) ;
#13817=AXIS2_PLACEMENT_3D ( 'NONE', #13846, #33113, #13677 ) ;
#13820=CYLINDRICAL_SURFACE ( 'NONE', #28432, 8.000000000000001776 ) ;
#13829=DIRECTION ( 'NONE',  ( 1.000000000000000000, -0.000000000000000000, -0.000000000000000000 ) ) ;
#13845=DIRECTION ( 'NONE',  ( 0.000000000000000000, 0.000000000000000000, 1.000000000000000000 ) ) ;
#13846=CARTESIAN_POINT ( 'NONE',  ( 0.000000000000000000, 0.000000000000000000, 0.000000000000000000 ) ) ;
#13849=CARTESIAN_POINT ( 'NONE',  ( 0.000000000000000000, -12.96676809804139197, -13.60411018104332292 ) ) ;
#13852=ORIENTED_EDGE ( 'NONE', *, *, #954, .F. ) ;
#13858=EDGE_LOOP ( 'NONE', ( #31665, #6964, #33204, #13816 ) ) ;
#13874=ORIENTED_EDGE ( 'NONE', *, *, #30112, .T. ) ;
#13879=EDGE_CURVE ( 'NONE', #25036, #26182, #34941, .T. ) ;
#13893=CIRCLE ( 'NONE', #13343, 8.000000000000003553 ) ;
#13895=AXIS2_PLACEMENT_3D ( 'NONE', #27344, #33436, #28052 ) ;
#13899=ORIENTED_EDGE ( 'NONE', *, *, #20482, .F. ) ;
#13918=AXIS2_PLACEMENT_3D ( 'NONE', #6426, #17574, #9313 ) ;
#13925=CARTESIAN_POINT ( 'NONE',  ( 8.000000000000000000, 16.94522934049215124, 8.128228055638924587 ) ) ;
#13931=AXIS2_PLACEMENT_3D ( 'NONE', #11945, #601, #11584 ) ;
#13932=CARTESIAN_POINT ( 'NONE',  ( 8.000000000000000000, -3.968388925834962500, 21.63912866391138934 ) ) ;
#13938=LINE ( 'NONE', #1315, #9357 ) ;
#13941=DIRECTION ( 'NONE',  ( 0.000000000000000000, 0.000000000000000000, 1.000000000000000000 ) ) ;
#13946=CIRCLE ( 'NONE', #3035, 22.00000000000000000 ) ;
#13983=DIRECTION ( 'NONE',  ( -1.000000000000000000, 0.000000000000000000, 0.000000000000000000 ) ) ;
#14015=DIRECTION ( 'NONE',  ( 0.000000000000000000, 0.000000000000000000, 1.000000000000000000 ) ) ;
#14024=ORIENTED_EDGE ( 'NONE', *, *, #4352, .F. ) ;
#14029=CARTESIAN_POINT ( 'NONE',  ( 8.000000000000000000, 3.384281271888069487, -18.48663108841355296 ) ) ;
#14064=CARTESIAN_POINT ( 'NONE',  ( 8.000000000000000000, -16.92083251265328769, 4.460989585140905156 ) ) ;
#14072=VERTEX_POINT ( 'NONE', #11462 ) ;
#14132=DIRECTION ( 'NONE',  ( 0.000000000000000000, 0.000000000000000000, 1.000000000000000000 ) ) ;
#14136=EDGE_CURVE ( 'NONE', #26858, #14835, #19547, .T. ) ;
#14144=DIRECTION ( 'NONE',  ( -1.000000000000000000, 0.000000000000000000, 0.000000000000000000 ) ) ;
#14147=DIRECTION ( 'NONE',  ( 0.000000000000000000, 0.8090169943749488946, -0.5877852522924709167 ) ) ;
#14151=CARTESIAN_POINT ( 'NONE',  ( 0.000000000000000000, 19.83898331853701080, -9.508666619816445120 ) ) ;
#14152=CARTESIAN_POINT ( 'NONE',  ( 0.000000000000000000, -18.48663108841356717, 4.615718728111985136 ) ) ;
#14155=VERTEX_POINT ( 'NONE', #17741 ) ;
#14161=EDGE_CURVE ( 'NONE', #21217, #34510, #14222, .T. ) ;
#14170=DIRECTION ( 'NONE',  ( 0.000000000000000000, 0.000000000000000000, 1.000000000000000000 ) ) ;
#14175=AXIS2_PLACEMENT_3D ( 'NONE', #8735, #14488, #12163 ) ;
#14190=LINE ( 'NONE', #25192, #9016 ) ;
#14210=CARTESIAN_POINT ( 'NONE',  ( 0.000000000000000000, -17.47118961583602470, 0.9861715913087032437 ) ) ;
#14217=DIRECTION ( 'NONE',  ( 1.000000000000000000, -0.000000000000000000, 0.000000000000000000 ) ) ;
#14222=CIRCLE ( 'NONE', #23342, 17.49900000000001299 ) ;
#14233=CARTESIAN_POINT ( 'NONE',  ( 0.000000000000000000, 8.931325931664597206, 16.53603053422209612 ) ) ;
#14234=VECTOR ( 'NONE', #24131, 1000.000000000000000 ) ;
#14238=DIRECTION ( 'NONE',  ( -1.000000000000000000, 0.000000000000000000, 0.000000000000000000 ) ) ;
#14256=EDGE_CURVE ( 'NONE', #17129, #26513, #8973, .T. ) ;
#14258=ORIENTED_EDGE ( 'NONE', *, *, #27407, .T. ) ;
#14259=EDGE_LOOP ( 'NONE', ( #23479, #25548, #5765, #31520 ) ) ;
#14273=DIRECTION ( 'NONE',  ( 0.000000000000000000, 0.000000000000000000, 1.000000000000000000 ) ) ;
#14274=CARTESIAN_POINT ( 'NONE',  ( 8.000000000000000000, 0.000000000000000000, 0.000000000000000000 ) ) ;
#14275=CARTESIAN_POINT ( 'NONE',  ( 8.000000000000000000, -21.63912866391141065, 3.968388925834729797 ) ) ;
#14285=AXIS2_PLACEMENT_3D ( 'NONE', #13790, #35592, #21343 ) ;
#14298=EDGE_CURVE ( 'NONE', #30312, #19686, #1372, .T. ) ;
#14304=DIRECTION ( 'NONE',  ( 0.000000000000000000, 0.000000000000000000, -1.000000000000000000 ) ) ;
#14311=AXIS2_PLACEMENT_3D ( 'NONE', #17493, #11928, #6345 ) ;
#14347=CARTESIAN_POINT ( 'NONE',  ( -10.00000000000000178, 0.000000000000000000, 0.000000000000000000 ) ) ;
#14368=AXIS2_PLACEMENT_3D ( 'NONE', #21725, #27849, #2669 ) ;
#14376=PRODUCT_DEFINITION_SHAPE ( 'NONE', 'NONE',  #18964 ) ;
#14390=DIRECTION ( 'NONE',  ( 0.000000000000000000, 0.000000000000000000, 1.000000000000000000 ) ) ;
#14404=FACE_OUTER_BOUND ( 'NONE', #32294, .T. ) ;
#14438=DIRECTION ( 'NONE',  ( 0.000000000000000000, 0.000000000000000000, 1.000000000000000000 ) ) ;
#14449=DIRECTION ( 'NONE',  ( -1.000000000000000000, 0.000000000000000000, 0.000000000000000000 ) ) ;
#14453=CYLINDRICAL_SURFACE ( 'NONE', #20533, 8.000000000000003553 ) ;
#14477=EDGE_CURVE ( 'NONE', #12175, #7742, #27980, .T. ) ;
#14483=EDGE_CURVE ( 'NONE', #9277, #24314, #10718, .T. ) ;
#14488=DIRECTION ( 'NONE',  ( -1.000000000000000000, 0.000000000000000000, 0.000000000000000000 ) ) ;
#14511=ORIENTED_EDGE ( 'NONE', *, *, #197, .T. ) ;
#14523=DIRECTION ( 'NONE',  ( -1.000000000000000000, 0.000000000000000000, 0.000000000000000000 ) ) ;
#14534=AXIS2_PLACEMENT_3D ( 'NONE', #13324, #21403, #26656 ) ;
#14545=EDGE_LOOP ( 'NONE', ( #7754, #22803, #9432, #6454 ) ) ;
#14560=EDGE_CURVE ( 'NONE', #11959, #27071, #35471, .T. ) ;
#14577=CYLINDRICAL_SURFACE ( 'NONE', #24472, 8.000000000000000000 ) ;
#14584=EDGE_LOOP ( 'NONE', ( #5543, #7087, #35434, #16645 ) ) ;
#14604=EDGE_LOOP ( 'NONE', ( #12954, #12356, #35565, #13017 ) ) ;
#14635=EDGE_CURVE ( 'NONE', #1616, #30950, #13780, .T. ) ;
#14638=DIRECTION ( 'NONE',  ( 0.000000000000000000, 0.3090169943749477288, -0.9510565162951534202 ) ) ;
#14648=AXIS2_PLACEMENT_3D ( 'NONE', #10337, #16607, #33353 ) ;
#14654=DIRECTION ( 'NONE',  ( 1.000000000000000000, -0.000000000000000000, -0.000000000000000000 ) ) ;
#14656=CARTESIAN_POINT ( 'NONE',  ( 8.000000000000000000, 8.128228055639098670, -16.94522934049206242 ) ) ;
#14668=CYLINDRICAL_SURFACE ( 'NONE', #20483, 22.00000000000000000 ) ;
#14677=AXIS2_PLACEMENT_3D ( 'NONE', #30422, #13680, #159 ) ;
#14696=AXIS2_PLACEMENT_3D ( 'NONE', #6625, #34010, #8968 ) ;
#14701=AXIS2_PLACEMENT_3D ( 'NONE', #27116, #2457, #13428 ) ;
#14707=DIRECTION ( 'NONE',  ( 0.000000000000000000, 0.000000000000000000, -1.000000000000000000 ) ) ;
#14729=DIRECTION ( 'NONE',  ( 0.000000000000000000, 0.000000000000000000, 1.000000000000000000 ) ) ;
#14731=EDGE_CURVE ( 'NONE', #21342, #30730, #3265, .T. ) ;
#14742=AXIS2_PLACEMENT_3D ( 'NONE', #7384, #32570, #15463 ) ;
#14752=AXIS2_PLACEMENT_3D ( 'NONE', #6228, #14144, #11618 ) ;
#14778=EDGE_CURVE ( 'NONE', #15404, #17296, #30274, .T. ) ;
#14798=ORIENTED_EDGE ( 'NONE', *, *, #22973, .F. ) ;
#14832=ORIENTED_EDGE ( 'NONE', *, *, #26194, .F. ) ;
#14835=VERTEX_POINT ( 'NONE', #21288 ) ;
#14836=ORIENTED_EDGE ( 'NONE', *, *, #25168, .T. ) ;
#14845=EDGE_CURVE ( 'NONE', #22897, #25036, #32643, .T. ) ;
#14850=VERTEX_POINT ( 'NONE', #31918 ) ;
#14854=CARTESIAN_POINT ( 'NONE',  ( 8.000000000000000000, -0.9861715913088822116, 17.47118961583599273 ) ) ;
#14855=CYLINDRICAL_SURFACE ( 'NONE', #30859, 8.000000000000000000 ) ;
#14856=AXIS2_PLACEMENT_3D ( 'NONE', #13754, #13570, #18786 ) ;
#14865=ORIENTED_EDGE ( 'NONE', *, *, #13092, .T. ) ;
#14875=SHAPE_DEFINITION_REPRESENTATION ( #14376, #8186 ) ;
#14952=AXIS2_PLACEMENT_3D ( 'NONE', #24832, #5746, #157 ) ;
#14972=EDGE_CURVE ( 'NONE', #25342, #26672, #17061, .T. ) ;
#14981=CIRCLE ( 'NONE', #23030, 8.000000000000007105 ) ;
#15032=ORIENTED_EDGE ( 'NONE', *, *, #13664, .T. ) ;
#15039=VERTEX_POINT ( 'NONE', #10863 ) ;
#15043=ORIENTED_EDGE ( 'NONE', *, *, #4421, .T. ) ;
#15053=CIRCLE ( 'NONE', #13918, 8.000000000000000000 ) ;
#15058=CYLINDRICAL_SURFACE ( 'NONE', #12501, 22.00000000000000000 ) ;
#15059=CARTESIAN_POINT ( 'NONE',  ( 0.000000000000000000, 19.35373470438985777, 10.46102064772347795 ) ) ;
#15106=FACE_OUTER_BOUND ( 'NONE', #11597, .T. ) ;
#15123=AXIS2_PLACEMENT_3D ( 'NONE', #4924, #32630, #32985 ) ;
#15127=VERTEX_POINT ( 'NONE', #11389 ) ;
#15139=CARTESIAN_POINT ( 'NONE',  ( 4.000000000000003553, -9.508666619816507293, -19.83898331853700370 ) ) ;
#15140=ORIENTED_EDGE ( 'NONE', *, *, #19598, .T. ) ;
#15146=DIRECTION ( 'NONE',  ( -1.000000000000000000, 0.000000000000000000, 0.000000000000000000 ) ) ;
#15152=AXIS2_PLACEMENT_3D ( 'NONE', #21314, #24049, #31949 ) ;
#15156=DIRECTION ( 'NONE',  ( 0.000000000000000000, 0.000000000000000000, -1.000000000000000000 ) ) ;
#15158=VERTEX_POINT ( 'NONE', #35536 ) ;
#15161=DIRECTION ( 'NONE',  ( 0.000000000000000000, -0.8090169943749533354, 0.5877852522924649215 ) ) ;
#15163=DIRECTION ( 'NONE',  ( 0.000000000000000000, -0.8090169943749405679, -0.5877852522924825740 ) ) ;
#15169=VERTEX_POINT ( 'NONE', #22354 ) ;
#15179=CARTESIAN_POINT ( 'NONE',  ( -10.00000000000000178, 0.000000000000000000, 0.000000000000000000 ) ) ;
#15196=AXIS2_PLACEMENT_3D ( 'NONE', #3387, #3030, #11467 ) ;
#15209=CARTESIAN_POINT ( 'NONE',  ( 0.000000000000000000, 3.384281271888069487, -18.48663108841355296 ) ) ;
#15221=ORIENTED_EDGE ( 'NONE', *, *, #17833, .F. ) ;
#15232=CIRCLE ( 'NONE', #3190, 17.49900000000001654 ) ;
#15249=CARTESIAN_POINT ( 'NONE',  ( 8.000000000000000000, 18.62763138773856397, -2.494040418455147456 ) ) ;
#15261=ORIENTED_EDGE ( 'NONE', *, *, #14161, .F. ) ;
#15262=AXIS2_PLACEMENT_3D ( 'NONE', #30500, #19497, #19834 ) ;
#15263=CIRCLE ( 'NONE', #4941, 22.00000000000000000 ) ;
#15283=CARTESIAN_POINT ( 'NONE',  ( 0.000000000000000000, -19.83898331853694685, 9.508666619816580123 ) ) ;
#15289=EDGE_CURVE ( 'NONE', #31693, #9081, #34606, .T. ) ;
#15294=AXIS2_PLACEMENT_3D ( 'NONE', #13258, #35225, #10374 ) ;
#15307=VERTEX_POINT ( 'NONE', #34434 ) ;
#15310=CIRCLE ( 'NONE', #3856, 17.49900000000001299 ) ;
#15311=AXIS2_PLACEMENT_3D ( 'NONE', #12927, #7349, #32008 ) ;
#15313=ORIENTED_EDGE ( 'NONE', *, *, #19173, .F. ) ;
#15338=CARTESIAN_POINT ( 'NONE',  ( 8.000000000000000000, 13.60411018104320036, 12.96676809804154118 ) ) ;
#15364=AXIS2_PLACEMENT_3D ( 'NONE', #22748, #3342, #14638 ) ;
#15373=DIRECTION ( 'NONE',  ( 0.000000000000000000, -1.000000000000000000, -1.047252562447196865E-14 ) ) ;
#15374=DIRECTION ( 'NONE',  ( 0.000000000000000000, 0.000000000000000000, 1.000000000000000000 ) ) ;
#15380=CYLINDRICAL_SURFACE ( 'NONE', #10923, 8.000000000000001776 ) ;
#15382=AXIS2_PLACEMENT_3D ( 'NONE', #5396, #18700, #15992 ) ;
#15385=CARTESIAN_POINT ( 'NONE',  ( 0.000000000000000000, 16.53603053422208902, -8.931325931664652273 ) ) ;
#15399=ORIENTED_EDGE ( 'NONE', *, *, #14136, .T. ) ;
#15404=VERTEX_POINT ( 'NONE', #2018 ) ;
#15414=AXIS2_PLACEMENT_3D ( 'NONE', #18785, #31982, #18963 ) ;
#15418=CARTESIAN_POINT ( 'NONE',  ( 8.000000000000000000, -13.60411018104326963, 12.96676809804144348 ) ) ;
#15426=DIRECTION ( 'NONE',  ( 1.000000000000000000, -0.000000000000000000, 0.000000000000000000 ) ) ;
#15444=EDGE_CURVE ( 'NONE', #33885, #29327, #29766, .T. ) ;
#15445=CARTESIAN_POINT ( 'NONE',  ( 0.000000000000000000, 4.898587196589412829E-16, -4.000000000000000000 ) ) ;
#15446=ORIENTED_EDGE ( 'NONE', *, *, #4602, .T. ) ;
#15463=DIRECTION ( 'NONE',  ( 0.000000000000000000, 0.000000000000000000, 1.000000000000000000 ) ) ;
#15467=LINE ( 'NONE', #20688, #23909 ) ;
#15488=CARTESIAN_POINT ( 'NONE',  ( 0.000000000000000000, 18.62763138773855687, 2.494040418455418351 ) ) ;
#15490=EDGE_CURVE ( 'NONE', #21171, #30484, #35526, .T. ) ;
#15504=CARTESIAN_POINT ( 'NONE',  ( 4.000000000000003553, -21.63912866391140710, 3.968388925834730685 ) ) ;
#15514=ORIENTED_EDGE ( 'NONE', *, *, #14845, .T. ) ;
#15538=CARTESIAN_POINT ( 'NONE',  ( 8.000000000000000000, 0.000000000000000000, 0.000000000000000000 ) ) ;
#15544=CARTESIAN_POINT ( 'NONE',  ( 8.000000000000000000, 0.000000000000000000, 0.000000000000000000 ) ) ;
#15551=CARTESIAN_POINT ( 'NONE',  ( 8.000000000000000000, -8.931325931664478190, -16.53603053422218494 ) ) ;
#15552=CARTESIAN_POINT ( 'NONE',  ( 0.000000000000000000, -18.48663108841356717, -3.384281271888017084 ) ) ;
#15604=VERTEX_POINT ( 'NONE', #3080 ) ;
#15609=ORIENTED_EDGE ( 'NONE', *, *, #20245, .T. ) ;
#15616=AXIS2_PLACEMENT_3D ( 'NONE', #22403, #24781, #3359 ) ;
#15618=DIRECTION ( 'NONE',  ( 0.000000000000000000, 1.000000000000000000, 3.469446951953613400E-15 ) ) ;
#15642=EDGE_LOOP ( 'NONE', ( #34144, #35223, #23686, #8069 ) ) ;
#15647=CIRCLE ( 'NONE', #34073, 17.49900000000001654 ) ;
#15654=LINE ( 'NONE', #18549, #9979 ) ;
#15685=AXIS2_PLACEMENT_3D ( 'NONE', #8592, #14523, #33816 ) ;
#15696=CIRCLE ( 'NONE', #9954, 8.000000000000001776 ) ;
#15733=VERTEX_POINT ( 'NONE', #15977 ) ;
#15743=ORIENTED_EDGE ( 'NONE', *, *, #34093, .F. ) ;
#15752=EDGE_LOOP ( 'NONE', ( #31879, #35232, #3241, #6375 ) ) ;
#15775=CARTESIAN_POINT ( 'NONE',  ( 0.000000000000000000, 18.48663108841356717, 3.384281271888136988 ) ) ;
#15810=LINE ( 'NONE', #35465, #23161 ) ;
#15812=CYLINDRICAL_SURFACE ( 'NONE', #21063, 17.49900000000000233 ) ;
#15822=EDGE_LOOP ( 'NONE', ( #20612, #13789, #27763, #1602 ) ) ;
#15838=ORIENTED_EDGE ( 'NONE', *, *, #15289, .T. ) ;
#15843=ORIENTED_EDGE ( 'NONE', *, *, #11481, .F. ) ;
#15889=AXIS2_PLACEMENT_3D ( 'NONE', #9786, #7079, #18054 ) ;
#15911=CARTESIAN_POINT ( 'NONE',  ( 8.000000000000000000, 9.471478019455355835, -14.71414642875945411 ) ) ;
#15921=CARTESIAN_POINT ( 'NONE',  ( 0.000000000000000000, 19.83898331853685448, 9.508666619816713350 ) ) ;
#15931=FACE_OUTER_BOUND ( 'NONE', #11036, .T. ) ;
#15937=EDGE_LOOP ( 'NONE', ( #9397, #25757, #30220, #12536 ) ) ;
#15945=ORIENTED_EDGE ( 'NONE', *, *, #28455, .F. ) ;
#15947=ADVANCED_FACE ( 'NONE', ( #10777 ), #27862, .T. ) ;
#15952=CARTESIAN_POINT ( 'NONE',  ( 8.000000000000000000, 18.62763138773855687, 10.49404041845541968 ) ) ;
#15958=AXIS2_PLACEMENT_3D ( 'NONE', #21213, #7882, #5026 ) ;
#15959=DIRECTION ( 'NONE',  ( -1.000000000000000000, 0.000000000000000000, 0.000000000000000000 ) ) ;
#15977=CARTESIAN_POINT ( 'NONE',  ( 0.000000000000000000, -15.17386234660395417, 15.92965478239613830 ) ) ;
#15978=AXIS2_PLACEMENT_3D ( 'NONE', #26109, #7010, #12060 ) ;
#15984=ADVANCED_FACE ( 'NONE', ( #22613 ), #4106, .T. ) ;
#15989=DIRECTION ( 'NONE',  ( 0.000000000000000000, 0.5877852522924682521, 0.8090169943749511150 ) ) ;
#15992=DIRECTION ( 'NONE',  ( 0.000000000000000000, 0.000000000000000000, 1.000000000000000000 ) ) ;
#15994=CARTESIAN_POINT ( 'NONE',  ( 4.000000000000003553, -15.17386234660395417, 15.92965478239613830 ) ) ;
#16019=DIRECTION ( 'NONE',  ( -1.000000000000000000, 0.000000000000000000, 0.000000000000000000 ) ) ;
#16069=CARTESIAN_POINT ( 'NONE',  ( 8.000000000000000000, 0.000000000000000000, 0.000000000000000000 ) ) ;
#16104=VECTOR ( 'NONE', #12692, 1000.000000000000000 ) ;
#16111=ORIENTED_EDGE ( 'NONE', *, *, #6207, .T. ) ;
#16140=EDGE_CURVE ( 'NONE', #12434, #3084, #12561, .T. ) ;
#16183=ADVANCED_FACE ( 'NONE', ( #5468 ), #24735, .T. ) ;
#16195=CARTESIAN_POINT ( 'NONE',  ( 0.000000000000000000, 4.460989585140964664, 16.92083251265327348 ) ) ;
#16226=DIRECTION ( 'NONE',  ( -1.000000000000000000, 0.000000000000000000, 0.000000000000000000 ) ) ;
#16243=CYLINDRICAL_SURFACE ( 'NONE', #4201, 8.000000000000001776 ) ;
#16253=VECTOR ( 'NONE', #7902, 1000.000000000000000 ) ;
#16266=CARTESIAN_POINT ( 'NONE',  ( 8.000000000000000000, 0.000000000000000000, 0.000000000000000000 ) ) ;
#16269=DIRECTION ( 'NONE',  ( -1.000000000000000000, 0.000000000000000000, 0.000000000000000000 ) ) ;
#16275=CARTESIAN_POINT ( 'NONE',  ( 8.000000000000000000, -8.128228055638727412, -16.94522934049221519 ) ) ;
#16285=DIRECTION ( 'NONE',  ( 0.000000000000000000, 0.000000000000000000, -1.000000000000000000 ) ) ;
#16287=AXIS2_PLACEMENT_3D ( 'NONE', #22112, #16533, #8775 ) ;
#16289=VERTEX_POINT ( 'NONE', #16612 ) ;
#16297=DIRECTION ( 'NONE',  ( 0.000000000000000000, 0.000000000000000000, -1.000000000000000000 ) ) ;
#16329=ORIENTED_EDGE ( 'NONE', *, *, #24199, .T. ) ;
#16362=AXIS2_PLACEMENT_3D ( 'NONE', #15209, #1557, #9119 ) ;
#16380=VERTEX_POINT ( 'NONE', #22012 ) ;
#16390=CARTESIAN_POINT ( 'NONE',  ( -10.00000000000000178, 0.000000000000000000, 0.000000000000000000 ) ) ;
#16393=LINE ( 'NONE', #33669, #28539 ) ;
#16394=VECTOR ( 'NONE', #25344, 1000.000000000000000 ) ;
#16395=CARTESIAN_POINT ( 'NONE',  ( 0.000000000000000000, 2.912696353505820124, 21.80633394113451473 ) ) ;
#16397=CARTESIAN_POINT ( 'NONE',  ( 8.000000000000000000, -8.931325931664478190, -16.53603053422218494 ) ) ;
#16451=DIRECTION ( 'NONE',  ( 0.000000000000000000, 0.8090169943749491166, -0.5877852522924710277 ) ) ;
#16452=CARTESIAN_POINT ( 'NONE',  ( 8.000000000000000000, 0.9861715913087641949, 17.47118961583602115 ) ) ;
#16467=ORIENTED_EDGE ( 'NONE', *, *, #2072, .T. ) ;
#16468=DIRECTION ( 'NONE',  ( 1.000000000000000000, -0.000000000000000000, -0.000000000000000000 ) ) ;
#16521=EDGE_CURVE ( 'NONE', #25573, #16289, #31363, .T. ) ;
#16522=CARTESIAN_POINT ( 'NONE',  ( 0.000000000000000000, -18.62763138773852134, 2.494040418455287345 ) ) ;
#16533=DIRECTION ( 'NONE',  ( -1.000000000000000000, 0.000000000000000000, 0.000000000000000000 ) ) ;
#16540=CARTESIAN_POINT ( 'NONE',  ( 0.000000000000000000, 0.000000000000000000, 0.000000000000000000 ) ) ;
#16568=ORIENTED_EDGE ( 'NONE', *, *, #14483, .T. ) ;
#16569=ORIENTED_EDGE ( 'NONE', *, *, #23143, .T. ) ;
#16592=VERTEX_POINT ( 'NONE', #27832 ) ;
#16598=ORIENTED_EDGE ( 'NONE', *, *, #10778, .F. ) ;
#16607=DIRECTION ( 'NONE',  ( -1.000000000000000000, 0.000000000000000000, 0.000000000000000000 ) ) ;
#16612=CARTESIAN_POINT ( 'NONE',  ( 0.000000000000000000, 16.92083251265334098, -4.460989585140788805 ) ) ;
#16615=FACE_OUTER_BOUND ( 'NONE', #7569, .T. ) ;
#16621=CARTESIAN_POINT ( 'NONE',  ( -10.00000000000000178, 0.000000000000000000, 0.000000000000000000 ) ) ;
#16623=ORIENTED_EDGE ( 'NONE', *, *, #5919, .T. ) ;
#16627=DIRECTION ( 'NONE',  ( 0.000000000000000000, 0.3090169943749477288, -0.9510565162951534202 ) ) ;
#16633=CARTESIAN_POINT ( 'NONE',  ( 8.000000000000000000, 0.000000000000000000, 0.000000000000000000 ) ) ;
#16643=VERTEX_POINT ( 'NONE', #20939 ) ;
#16645=ORIENTED_EDGE ( 'NONE', *, *, #232, .T. ) ;
#16647=VERTEX_POINT ( 'NONE', #12322 ) ;
#16651=DIRECTION ( 'NONE',  ( 0.000000000000000000, 0.000000000000000000, 1.000000000000000000 ) ) ;
#16675=VECTOR ( 'NONE', #21407, 1000.000000000000000 ) ;
#16683=CIRCLE ( 'NONE', #1177, 22.00000000000000000 ) ;
#16689=LINE ( 'NONE', #10956, #25981 ) ;
#16691=VERTEX_POINT ( 'NONE', #4416 ) ;
#16700=DIRECTION ( 'NONE',  ( -1.000000000000000000, 0.000000000000000000, 0.000000000000000000 ) ) ;
#16711=ORIENTED_EDGE ( 'NONE', *, *, #10818, .T. ) ;
#16730=ADVANCED_FACE ( 'NONE', ( #18251 ), #29255, .T. ) ;
#16749=DIRECTION ( 'NONE',  ( 0.000000000000000000, 0.000000000000000000, -1.000000000000000000 ) ) ;
#16777=ORIENTED_EDGE ( 'NONE', *, *, #6183, .F. ) ;
#16793=ADVANCED_BREP_SHAPE_REPRESENTATION ( '', ( #10370, #21307 ), #30547 ) ;
#16795=DIRECTION ( 'NONE',  ( -1.000000000000000000, 0.000000000000000000, 0.000000000000000000 ) ) ;
#16813=CARTESIAN_POINT ( 'NONE',  ( 8.000000000000000000, 0.000000000000000000, 0.000000000000000000 ) ) ;
#16815=ORIENTED_EDGE ( 'NONE', *, *, #30436, .F. ) ;
#16825=FACE_OUTER_BOUND ( 'NONE', #24600, .T. ) ;
#16845=ORIENTED_EDGE ( 'NONE', *, *, #11946, .T. ) ;
#16858=ORIENTED_EDGE ( 'NONE', *, *, #831, .T. ) ;
#16866=FACE_OUTER_BOUND ( 'NONE', #25242, .T. ) ;
#16885=EDGE_LOOP ( 'NONE', ( #25388, #2692, #19421, #18175 ) ) ;
#16886=EDGE_CURVE ( 'NONE', #5380, #30763, #12014, .T. ) ;
#16902=EDGE_CURVE ( 'NONE', #30814, #5963, #8541, .T. ) ;
#16911=EDGE_CURVE ( 'NONE', #7954, #30484, #19134, .T. ) ;
#16921=AXIS2_PLACEMENT_3D ( 'NONE', #9329, #34538, #20285 ) ;
#16930=VERTEX_POINT ( 'NONE', #3130 ) ;
#16941=ORIENTED_EDGE ( 'NONE', *, *, #33855, .F. ) ;
#16956=EDGE_CURVE ( 'NONE', #15169, #26218, #19822, .T. ) ;
#16964=CIRCLE ( 'NONE', #31376, 22.00000000000000000 ) ;
#16965=CARTESIAN_POINT ( 'NONE',  ( 8.000000000000000000, 9.471478019455355835, -14.71414642875945411 ) ) ;
#16981=AXIS2_PLACEMENT_3D ( 'NONE', #12172, #17021, #23145 ) ;
#16990=EDGE_CURVE ( 'NONE', #24314, #27865, #24113, .T. ) ;
#17001=DIRECTION ( 'NONE',  ( -1.000000000000000000, 0.000000000000000000, 0.000000000000000000 ) ) ;
#17014=AXIS2_PLACEMENT_3D ( 'NONE', #11797, #20239, #472 ) ;
#17015=CARTESIAN_POINT ( 'NONE',  ( 8.000000000000000000, -0.9861715913086367413, -17.47118961583605312 ) ) ;
#17021=DIRECTION ( 'NONE',  ( -1.000000000000000000, 0.000000000000000000, 0.000000000000000000 ) ) ;
#17025=ORIENTED_EDGE ( 'NONE', *, *, #18767, .F. ) ;
#17034=AXIS2_PLACEMENT_3D ( 'NONE', #20377, #6369, #3868 ) ;
#17058=AXIS2_PLACEMENT_3D ( 'NONE', #12068, #12251, #34580 ) ;
#17061=CIRCLE ( 'NONE', #13643, 8.000000000000007105 ) ;
#17082=CIRCLE ( 'NONE', #21698, 22.00000000000000000 ) ;
#17091=ORIENTED_EDGE ( 'NONE', *, *, #8909, .F. ) ;
#17092=AXIS2_PLACEMENT_3D ( 'NONE', #16813, #17163, #6372 ) ;
#17110=ORIENTED_EDGE ( 'NONE', *, *, #5137, .F. ) ;
#17123=ORIENTED_EDGE ( 'NONE', *, *, #3455, .T. ) ;
#17128=DIRECTION ( 'NONE',  ( -1.000000000000000000, 0.000000000000000000, 0.000000000000000000 ) ) ;
#17129=VERTEX_POINT ( 'NONE', #25806 ) ;
#17163=DIRECTION ( 'NONE',  ( -1.000000000000000000, 0.000000000000000000, 0.000000000000000000 ) ) ;
#17179=CARTESIAN_POINT ( 'NONE',  ( 8.000000000000000000, 13.60411018104336023, -12.96676809804134400 ) ) ;
#17186=VECTOR ( 'NONE', #27597, 1000.000000000000000 ) ;
#17200=DIRECTION ( 'NONE',  ( -1.000000000000000000, 0.000000000000000000, 0.000000000000000000 ) ) ;
#17220=ORIENTED_EDGE ( 'NONE', *, *, #8396, .T. ) ;
#17230=DIRECTION ( 'NONE',  ( 1.000000000000000000, -0.000000000000000000, 0.000000000000000000 ) ) ;
#17235=CARTESIAN_POINT ( 'NONE',  ( 8.000000000000000000, 0.000000000000000000, 0.000000000000000000 ) ) ;
#17263=ORIENTED_EDGE ( 'NONE', *, *, #31047, .F. ) ;
#17264=AXIS2_PLACEMENT_3D ( 'NONE', #7679, #23540, #12382 ) ;
#17296=VERTEX_POINT ( 'NONE', #2391 ) ;
#17297=VECTOR ( 'NONE', #18689, 1000.000000000000000 ) ;
#17311=CARTESIAN_POINT ( 'NONE',  ( 8.000000000000000000, 16.92083251265325572, 4.460989585141031277 ) ) ;
#17336=CARTESIAN_POINT ( 'NONE',  ( 8.000000000000000000, 14.71414642875954648, 9.471478019455206621 ) ) ;
#17354=CYLINDRICAL_SURFACE ( 'NONE', #26412, 17.49900000000000233 ) ;
#17362=ORIENTED_EDGE ( 'NONE', *, *, #14972, .T. ) ;
#17380=CIRCLE ( 'NONE', #28917, 17.49900000000001654 ) ;
#17382=LINE ( 'NONE', #3726, #1567 ) ;
#17404=AXIS2_PLACEMENT_3D ( 'NONE', #15544, #26563, #12155 ) ;
#17413=CARTESIAN_POINT ( 'NONE',  ( 8.000000000000000000, -19.83898331853678343, -9.508666619816857235 ) ) ;
#17437=EDGE_CURVE ( 'NONE', #3084, #5415, #23552, .T. ) ;
#17443=VECTOR ( 'NONE', #23968, 1000.000000000000000 ) ;
#17444=AXIS2_PLACEMENT_3D ( 'NONE', #25857, #1184, #11614 ) ;
#17462=CARTESIAN_POINT ( 'NONE',  ( 8.000000000000000000, 15.92965478239641008, -15.17386234660365751 ) ) ;
#17491=ORIENTED_EDGE ( 'NONE', *, *, #12316, .F. ) ;
#17493=CARTESIAN_POINT ( 'NONE',  ( 0.000000000000000000, -18.62763138773852134, 2.494040418455287345 ) ) ;
#17495=CIRCLE ( 'NONE', #4885, 4.000000000000000000 ) ;
#17503=ORIENTED_EDGE ( 'NONE', *, *, #21565, .F. ) ;
#17523=EDGE_LOOP ( 'NONE', ( #30466, #8701, #21068, #10630 ) ) ;
#17554=CARTESIAN_POINT ( 'NONE',  ( 0.000000000000000000, 0.000000000000000000, -1.000000000000000222 ) ) ;
#17562=DIRECTION ( 'NONE',  ( -1.000000000000000000, 0.000000000000000000, 0.000000000000000000 ) ) ;
#17571=VERTEX_POINT ( 'NONE', #147 ) ;
#17574=DIRECTION ( 'NONE',  ( -1.000000000000000000, 0.000000000000000000, 0.000000000000000000 ) ) ;
#17580=CIRCLE ( 'NONE', #6083, 17.49900000000001654 ) ;
#17584=DIRECTION ( 'NONE',  ( 0.000000000000000000, 0.000000000000000000, 1.000000000000000000 ) ) ;
#17600=EDGE_LOOP ( 'NONE', ( #4566, #26003, #2829, #6485 ) ) ;
#17606=ORIENTED_EDGE ( 'NONE', *, *, #23202, .F. ) ;
#17619=ORIENTED_EDGE ( 'NONE', *, *, #232, .F. ) ;
#17655=EDGE_CURVE ( 'NONE', #26672, #34739, #13793, .T. ) ;
#17730=DIRECTION ( 'NONE',  ( -1.000000000000000000, 0.000000000000000000, 0.000000000000000000 ) ) ;
#17738=ORIENTED_EDGE ( 'NONE', *, *, #34342, .T. ) ;
#17741=CARTESIAN_POINT ( 'NONE',  ( 0.000000000000000000, 13.55483219355729396, 11.06713717293245658 ) ) ;
#17772=CARTESIAN_POINT ( 'NONE',  ( 8.000000000000000000, -18.62763138773852134, 10.49404041845529001 ) ) ;
#17789=VECTOR ( 'NONE', #17979, 1000.000000000000000 ) ;
#17799=AXIS2_PLACEMENT_3D ( 'NONE', #23488, #28892, #1707 ) ;
#17811=AXIS2_PLACEMENT_3D ( 'NONE', #13316, #2174, #10433 ) ;
#17817=ADVANCED_FACE ( 'NONE', ( #9317 ), #34348, .T. ) ;
#17833=EDGE_CURVE ( 'NONE', #180, #23058, #11828, .T. ) ;
#17860=UNCERTAINTY_MEASURE_WITH_UNIT (LENGTH_MEASURE( 1.000000000000000082E-05 ), #34474, 'distance_accuracy_value', 'NONE');
#17874=DIRECTION ( 'NONE',  ( 0.000000000000000000, 0.000000000000000000, -1.000000000000000000 ) ) ;
#17877=VERTEX_POINT ( 'NONE', #27138 ) ;
#17900=DIRECTION ( 'NONE',  ( -1.000000000000000000, 0.000000000000000000, 0.000000000000000000 ) ) ;
#17902=EDGE_CURVE ( 'NONE', #272, #30478, #7671, .T. ) ;
#17935=EDGE_CURVE ( 'NONE', #8636, #24798, #17082, .T. ) ;
#17941=DIRECTION ( 'NONE',  ( 0.000000000000000000, 0.000000000000000000, 1.000000000000000000 ) ) ;
#17948=CYLINDRICAL_SURFACE ( 'NONE', #24775, 8.000000000000000000 ) ;
#17966=VERTEX_POINT ( 'NONE', #4992 ) ;
#17973=CIRCLE ( 'NONE', #3636, 22.00000000000000000 ) ;
#17976=EDGE_CURVE ( 'NONE', #3480, #5736, #6181, .T. ) ;
#17979=DIRECTION ( 'NONE',  ( -1.000000000000000000, 0.000000000000000000, 0.000000000000000000 ) ) ;
#18021=EDGE_LOOP ( 'NONE', ( #8671, #7033, #4717, #11723 ) ) ;
#18052=EDGE_CURVE ( 'NONE', #519, #32655, #4484, .T. ) ;
#18054=DIRECTION ( 'NONE',  ( 0.000000000000000000, 0.000000000000000000, 1.000000000000000000 ) ) ;
#18061=ORIENTED_EDGE ( 'NONE', *, *, #31055, .F. ) ;
#18083=ORIENTED_EDGE ( 'NONE', *, *, #13107, .F. ) ;
#18084=DIRECTION ( 'NONE',  ( 0.000000000000000000, 0.000000000000000000, 1.000000000000000000 ) ) ;
#18099=ADVANCED_FACE ( 'NONE', ( #24785 ), #11443, .T. ) ;
#18105=ORIENTED_EDGE ( 'NONE', *, *, #27920, .F. ) ;
#18140=ORIENTED_EDGE ( 'NONE', *, *, #21601, .T. ) ;
#18169=DIRECTION ( 'NONE',  ( 0.000000000000000000, 0.9510565162951523099, 0.3090169943749513370 ) ) ;
#18175=ORIENTED_EDGE ( 'NONE', *, *, #2261, .T. ) ;
#18178=VERTEX_POINT ( 'NONE', #19695 ) ;
#18182=VECTOR ( 'NONE', #19852, 1000.000000000000000 ) ;
#18229=EDGE_CURVE ( 'NONE', #34100, #7117, #23299, .T. ) ;
#18251=FACE_OUTER_BOUND ( 'NONE', #9838, .T. ) ;
#18269=LINE ( 'NONE', #2097, #4936 ) ;
#18270=ADVANCED_FACE ( 'NONE', ( #23994 ), #28538, .T. ) ;
#18278=DIRECTION ( 'NONE',  ( -1.000000000000000000, 0.000000000000000000, 0.000000000000000000 ) ) ;
#18280=DIRECTION ( 'NONE',  ( 0.000000000000000000, 0.000000000000000000, -1.000000000000000000 ) ) ;
#18282=ORIENTED_EDGE ( 'NONE', *, *, #30318, .T. ) ;
#18289=ORIENTED_EDGE ( 'NONE', *, *, #28388, .F. ) ;
#18292=DIRECTION ( 'NONE',  ( 1.000000000000000000, 0.000000000000000000, 0.000000000000000000 ) ) ;
#18299=CARTESIAN_POINT ( 'NONE',  ( 8.000000000000000000, -19.83898331853694685, 9.508666619816578347 ) ) ;
#18300=DIRECTION ( 'NONE',  ( -1.000000000000000000, 0.000000000000000000, 0.000000000000000000 ) ) ;
#18301=VECTOR ( 'NONE', #10265, 1000.000000000000000 ) ;
#18314=DIRECTION ( 'NONE',  ( -1.000000000000000000, 0.000000000000000000, 0.000000000000000000 ) ) ;
#18317=CARTESIAN_POINT ( 'NONE',  ( 8.000000000000000000, 8.931325931664870765, -16.53603053422199665 ) ) ;
#18319=DIRECTION ( 'NONE',  ( 0.000000000000000000, 0.000000000000000000, 1.000000000000000000 ) ) ;
#18332=ORIENTED_EDGE ( 'NONE', *, *, #19909, .T. ) ;
#18341=ORIENTED_EDGE ( 'NONE', *, *, #31040, .F. ) ;
#18345=FACE_OUTER_BOUND ( 'NONE', #14604, .T. ) ;
#18352=DIRECTION ( 'NONE',  ( 0.000000000000000000, 1.000000000000000000, 3.491564676272318479E-15 ) ) ;
#18381=DIRECTION ( 'NONE',  ( -1.000000000000000000, 0.000000000000000000, 0.000000000000000000 ) ) ;
#18382=CYLINDRICAL_SURFACE ( 'NONE', #20738, 22.00000000000000000 ) ;
#18385=AXIS2_PLACEMENT_3D ( 'NONE', #30746, #671, #8247 ) ;
#18387=CARTESIAN_POINT ( 'NONE',  ( 0.000000000000000000, 11.06713717293239441, 13.55483219355733837 ) ) ;
#18404=CARTESIAN_POINT ( 'NONE',  ( 8.000000000000000000, 0.000000000000000000, 0.000000000000000000 ) ) ;
#18415=DIRECTION ( 'NONE',  ( 0.000000000000000000, -0.3090169943749547787, 0.9510565162951513107 ) ) ;
#18419=CYLINDRICAL_SURFACE ( 'NONE', #25516, 8.000000000000000000 ) ;
#18421=EDGE_LOOP ( 'NONE', ( #19448, #1202, #28938, #21985 ) ) ;
#18428=DIRECTION ( 'NONE',  ( 0.000000000000000000, 0.000000000000000000, 1.000000000000000000 ) ) ;
#18439=DIRECTION ( 'NONE',  ( 0.000000000000000000, -0.3090169943749545567, 0.9510565162951513107 ) ) ;
#18447=CARTESIAN_POINT ( 'NONE',  ( 0.000000000000000000, 21.63912866391145684, -3.968388925834583247 ) ) ;
#18452=CARTESIAN_POINT ( 'NONE',  ( 8.000000000000000000, 0.000000000000000000, 0.000000000000000000 ) ) ;
#18459=ORIENTED_EDGE ( 'NONE', *, *, #9904, .F. ) ;
#18472=CARTESIAN_POINT ( 'NONE',  ( 4.000000000000003553, 9.508666619816942500, -19.83898331853677632 ) ) ;
#18477=PLANE ( 'NONE',  #27169 ) ;
#18491=EDGE_CURVE ( 'NONE', #21764, #14072, #30097, .T. ) ;
#18532=CARTESIAN_POINT ( 'NONE',  ( 8.000000000000000000, 3.384281271887823461, 18.48663108841358138 ) ) ;
#18538=LINE ( 'NONE', #13503, #20336 ) ;
#18549=CARTESIAN_POINT ( 'NONE',  ( 8.000000000000000000, 16.31134495048485178, 6.336799421339877725 ) ) ;
#18557=DIRECTION ( 'NONE',  ( 0.000000000000000000, -0.8090169943749405679, -0.5877852522924827960 ) ) ;
#18558=ORIENTED_EDGE ( 'NONE', *, *, #22857, .T. ) ;
#18562=CARTESIAN_POINT ( 'NONE',  ( 8.000000000000000000, -2.912696353505664248, -21.80633394113455736 ) ) ;
#18581=CARTESIAN_POINT ( 'NONE',  ( 0.000000000000000000, -6.336799421339700977, -16.31134495048491573 ) ) ;
#18585=DIRECTION ( 'NONE',  ( 0.000000000000000000, -0.9510565162951564178, 0.3090169943749385140 ) ) ;
#18589=AXIS2_PLACEMENT_3D ( 'NONE', #3279, #14238, #30290 ) ;
#18615=DIRECTION ( 'NONE',  ( -1.000000000000000000, 0.000000000000000000, 0.000000000000000000 ) ) ;
#18627=ORIENTED_EDGE ( 'NONE', *, *, #20257, .F. ) ;
#18664=CARTESIAN_POINT ( 'NONE',  ( 0.000000000000000000, 0.000000000000000000, 0.000000000000000000 ) ) ;
#18667=DIRECTION ( 'NONE',  ( 0.000000000000000000, 0.000000000000000000, -1.000000000000000000 ) ) ;
#18689=DIRECTION ( 'NONE',  ( -1.000000000000000000, 0.000000000000000000, 0.000000000000000000 ) ) ;
#18700=DIRECTION ( 'NONE',  ( -1.000000000000000000, 0.000000000000000000, 0.000000000000000000 ) ) ;
#18719=EDGE_CURVE ( 'NONE', #1616, #8203, #22310, .T. ) ;
#18722=ADVANCED_FACE ( 'NONE', ( #31676 ), #9540, .T. ) ;
#18728=CARTESIAN_POINT ( 'NONE',  ( 8.000000000000000000, -19.35373470438975119, -10.46102064772362183 ) ) ;
#18739=DIRECTION ( 'NONE',  ( 0.000000000000000000, 0.9510565162951544194, -0.3090169943749448977 ) ) ;
#18742=CIRCLE ( 'NONE', #7793, 17.49900000000000233 ) ;
#18762=DIRECTION ( 'NONE',  ( -1.000000000000000000, 0.000000000000000000, 0.000000000000000000 ) ) ;
#18767=EDGE_CURVE ( 'NONE', #34183, #29017, #28058, .T. ) ;
#18771=VERTEX_POINT ( 'NONE', #23580 ) ;
#18783=ORIENTED_EDGE ( 'NONE', *, *, #30564, .F. ) ;
#18785=CARTESIAN_POINT ( 'NONE',  ( 8.000000000000000000, 0.000000000000000000, 0.000000000000000000 ) ) ;
#18786=DIRECTION ( 'NONE',  ( 0.000000000000000000, 0.000000000000000000, 1.000000000000000000 ) ) ;
#18788=CARTESIAN_POINT ( 'NONE',  ( 0.000000000000000000, 0.000000000000000000, 0.000000000000000000 ) ) ;
#18792=CARTESIAN_POINT ( 'NONE',  ( 0.000000000000000000, 0.000000000000000000, 0.000000000000000000 ) ) ;
#18796=EDGE_CURVE ( 'NONE', #25838, #9043, #34573, .T. ) ;
#18797=FACE_OUTER_BOUND ( 'NONE', #15822, .T. ) ;
#18803=VERTEX_POINT ( 'NONE', #7380 ) ;
#18813=LINE ( 'NONE', #29814, #21855 ) ;
#18816=ORIENTED_EDGE ( 'NONE', *, *, #7988, .F. ) ;
#18819=CARTESIAN_POINT ( 'NONE',  ( 0.000000000000000000, -3.384281271887680909, -18.48663108841362757 ) ) ;
#18823=EDGE_LOOP ( 'NONE', ( #23435, #7133, #2250, #2826 ) ) ;
#18827=EDGE_LOOP ( 'NONE', ( #25952, #23391, #4876, #2778 ) ) ;
#18829=VECTOR ( 'NONE', #9924, 1000.000000000000000 ) ;
#18832=CIRCLE ( 'NONE', #17092, 22.00000000000000000 ) ;
#18840=CARTESIAN_POINT ( 'NONE',  ( 8.000000000000000000, 0.000000000000000000, 0.000000000000000000 ) ) ;
#18841=CARTESIAN_POINT ( 'NONE',  ( 8.000000000000000000, 13.60411018104320036, 12.96676809804154118 ) ) ;
#18871=CARTESIAN_POINT ( 'NONE',  ( 8.000000000000000000, -13.55483219355720337, -11.06713717293254362 ) ) ;
#18877=CYLINDRICAL_SURFACE ( 'NONE', #17811, 8.000000000000000000 ) ;
#18884=ADVANCED_FACE ( 'NONE', ( #32398 ), #5048, .T. ) ;
#18939=ORIENTED_EDGE ( 'NONE', *, *, #4442, .T. ) ;
#18943=CARTESIAN_POINT ( 'NONE',  ( 0.000000000000000000, 0.000000000000000000, 0.000000000000000000 ) ) ;
#18944=CIRCLE ( 'NONE', #31001, 17.49900000000001654 ) ;
#18951=ORIENTED_EDGE ( 'NONE', *, *, #22497, .F. ) ;
#18963=DIRECTION ( 'NONE',  ( 0.000000000000000000, 0.000000000000000000, 1.000000000000000000 ) ) ;
#18964=PRODUCT_DEFINITION ( 'UNKNOWN', '', #32764, #28142 ) ;
#18976=CIRCLE ( 'NONE', #34513, 22.00000000000000000 ) ;
#18977=CARTESIAN_POINT ( 'NONE',  ( 0.000000000000000000, -16.92083251265328769, 4.460989585140905156 ) ) ;
#18986=EDGE_CURVE ( 'NONE', #30814, #34436, #12961, .T. ) ;
#18990=LINE ( 'NONE', #13419, #28597 ) ;
#18991=DIRECTION ( 'NONE',  ( 0.000000000000000000, 0.000000000000000000, 1.000000000000000000 ) ) ;
#19001=ORIENTED_EDGE ( 'NONE', *, *, #25082, .T. ) ;
#19006=DIRECTION ( 'NONE',  ( 1.000000000000000000, -0.000000000000000000, 0.000000000000000000 ) ) ;
#19008=ADVANCED_FACE ( 'NONE', ( #26051 ), #4811, .T. ) ;
#19014=DIRECTION ( 'NONE',  ( 0.000000000000000000, 0.000000000000000000, 1.000000000000000000 ) ) ;
#19015=DIRECTION ( 'NONE',  ( 0.000000000000000000, 0.8090169943749488946, -0.5877852522924709167 ) ) ;
#19028=( NAMED_UNIT ( * ) SI_UNIT ( $, .STERADIAN. ) SOLID_ANGLE_UNIT ( ) );
#19044=AXIS2_PLACEMENT_3D ( 'NONE', #24787, #13281, #32350 ) ;
#19087=DIRECTION ( 'NONE',  ( -1.000000000000000000, 0.000000000000000000, 0.000000000000000000 ) ) ;
#19108=LINE ( 'NONE', #35519, #17186 ) ;
#19109=CARTESIAN_POINT ( 'NONE',  ( 0.000000000000000000, 0.000000000000000000, 0.000000000000000000 ) ) ;
#19125=ORIENTED_EDGE ( 'NONE', *, *, #31080, .F. ) ;
#19134=LINE ( 'NONE', #11050, #5722 ) ;
#19166=LINE ( 'NONE', #13782, #2101 ) ;
#19171=EDGE_CURVE ( 'NONE', #30052, #4766, #7489, .T. ) ;
#19173=EDGE_CURVE ( 'NONE', #1617, #9760, #13717, .T. ) ;
#19197=CIRCLE ( 'NONE', #7147, 8.000000000000001776 ) ;
#19206=VERTEX_POINT ( 'NONE', #26958 ) ;
#19247=CARTESIAN_POINT ( 'NONE',  ( 4.000000000000003553, -21.63912866391137868, -3.968388925835035330 ) ) ;
#19250=CIRCLE ( 'NONE', #2604, 8.000000000000007105 ) ;
#19258=DIRECTION ( 'NONE',  ( 1.000000000000000000, -0.000000000000000000, -0.000000000000000000 ) ) ;
#19277=EDGE_CURVE ( 'NONE', #6546, #251, #495, .T. ) ;
#19281=CYLINDRICAL_SURFACE ( 'NONE', #18589, 22.00000000000000000 ) ;
#19282=AXIS2_PLACEMENT_3D ( 'NONE', #9782, #25196, #8084 ) ;
#19294=ORIENTED_EDGE ( 'NONE', *, *, #32404, .F. ) ;
#19316=ADVANCED_FACE ( 'NONE', ( #30359 ), #32508, .T. ) ;
#19318=EDGE_CURVE ( 'NONE', #7742, #15404, #5169, .T. ) ;
#19338=VERTEX_POINT ( 'NONE', #11970 ) ;
#19358=CARTESIAN_POINT ( 'NONE',  ( 8.000000000000000000, 0.000000000000000000, 0.000000000000000000 ) ) ;
#19371=CARTESIAN_POINT ( 'NONE',  ( 8.000000000000000000, 0.000000000000000000, 4.000000000000000000 ) ) ;
#19380=LINE ( 'NONE', #27686, #3285 ) ;
#19389=CARTESIAN_POINT ( 'NONE',  ( 8.000000000000000000, -6.336799421339700977, -16.31134495048491573 ) ) ;
#19392=AXIS2_PLACEMENT_3D ( 'NONE', #2108, #13083, #2289 ) ;
#19419=FACE_OUTER_BOUND ( 'NONE', #28524, .T. ) ;
#19421=ORIENTED_EDGE ( 'NONE', *, *, #31080, .T. ) ;
#19434=ORIENTED_EDGE ( 'NONE', *, *, #3703, .T. ) ;
#19436=DIRECTION ( 'NONE',  ( -1.000000000000000000, 0.000000000000000000, 0.000000000000000000 ) ) ;
#19447=CARTESIAN_POINT ( 'NONE',  ( 8.000000000000000000, -4.460989585140847424, -16.92083251265332322 ) ) ;
#19448=ORIENTED_EDGE ( 'NONE', *, *, #32426, .F. ) ;
#19470=CYLINDRICAL_SURFACE ( 'NONE', #12844, 22.00000000000000000 ) ;
#19472=CARTESIAN_POINT ( 'NONE',  ( 0.000000000000000000, 18.62763138773855687, 2.494040418455418351 ) ) ;
#19493=DIRECTION ( 'NONE',  ( 0.000000000000000000, 0.000000000000000000, 1.000000000000000000 ) ) ;
#19497=DIRECTION ( 'NONE',  ( -1.000000000000000000, 0.000000000000000000, 0.000000000000000000 ) ) ;
#19498=DIRECTION ( 'NONE',  ( 0.000000000000000000, 0.000000000000000000, 1.000000000000000000 ) ) ;
#19499=ORIENTED_EDGE ( 'NONE', *, *, #13327, .F. ) ;
#19519=EDGE_LOOP ( 'NONE', ( #29864, #5118, #20832, #24447 ) ) ;
#19540=( LENGTH_UNIT ( ) NAMED_UNIT ( * ) SI_UNIT ( .MILLI., .METRE. ) );
#19547=LINE ( 'NONE', #20072, #9629 ) ;
#19553=ORIENTED_EDGE ( 'NONE', *, *, #2077, .T. ) ;
#19565=EDGE_CURVE ( 'NONE', #18178, #24515, #18944, .T. ) ;
#19569=EDGE_CURVE ( 'NONE', #24798, #16647, #21791, .T. ) ;
#19598=EDGE_CURVE ( 'NONE', #13434, #34100, #22944, .T. ) ;
#19606=CARTESIAN_POINT ( 'NONE',  ( 0.000000000000000000, 12.96676809804150565, 13.60411018104323411 ) ) ;
#19661=FACE_OUTER_BOUND ( 'NONE', #7537, .T. ) ;
#19672=FACE_OUTER_BOUND ( 'NONE', #2948, .T. ) ;
#19686=VERTEX_POINT ( 'NONE', #11098 ) ;
#19688=AXIS2_PLACEMENT_3D ( 'NONE', #14656, #33577, #33406 ) ;
#19695=CARTESIAN_POINT ( 'NONE',  ( 0.000000000000000000, -4.460989585140847424, -16.92083251265332322 ) ) ;
#19705=CARTESIAN_POINT ( 'NONE',  ( 0.000000000000000000, 0.000000000000000000, 0.000000000000000000 ) ) ;
#19723=EDGE_CURVE ( 'NONE', #1815, #15127, #23522, .T. ) ;
#19745=DIRECTION ( 'NONE',  ( -1.000000000000000000, 0.000000000000000000, 0.000000000000000000 ) ) ;
#19759=DIRECTION ( 'NONE',  ( -1.000000000000000000, 0.000000000000000000, 0.000000000000000000 ) ) ;
#19775=ORIENTED_EDGE ( 'NONE', *, *, #3862, .F. ) ;
#19784=DIRECTION ( 'NONE',  ( -1.000000000000000000, 0.000000000000000000, -0.000000000000000000 ) ) ;
#19792=EDGE_CURVE ( 'NONE', #24314, #25036, #5720, .T. ) ;
#19793=CARTESIAN_POINT ( 'NONE',  ( 8.000000000000000000, 13.55483219355729396, 11.06713717293245658 ) ) ;
#19797=CARTESIAN_POINT ( 'NONE',  ( -10.00000000000000178, 0.000000000000000000, 0.000000000000000000 ) ) ;
#19821=ORIENTED_EDGE ( 'NONE', *, *, #282, .F. ) ;
#19822=LINE ( 'NONE', #17311, #28704 ) ;
#19834=DIRECTION ( 'NONE',  ( 0.000000000000000000, -0.8090169943749533354, 0.5877852522924649215 ) ) ;
#19836=ADVANCED_FACE ( 'NONE', ( #28186 ), #17354, .T. ) ;
#19839=EDGE_CURVE ( 'NONE', #4766, #34692, #4583, .T. ) ;
#19852=DIRECTION ( 'NONE',  ( -1.000000000000000000, 0.000000000000000000, 0.000000000000000000 ) ) ;
#19868=DIRECTION ( 'NONE',  ( -1.000000000000000000, 0.000000000000000000, 0.000000000000000000 ) ) ;
#19895=AXIS2_PLACEMENT_3D ( 'NONE', #19797, #11900, #25241 ) ;
#19907=ORIENTED_EDGE ( 'NONE', *, *, #31972, .F. ) ;
#19909=EDGE_CURVE ( 'NONE', #27440, #12176, #33574, .T. ) ;
#19920=CARTESIAN_POINT ( 'NONE',  ( 8.000000000000000000, 10.46102064772367868, -19.35373470438973698 ) ) ;
#19930=AXIS2_PLACEMENT_3D ( 'NONE', #31601, #23313, #31956 ) ;
#19957=EDGE_CURVE ( 'NONE', #14155, #21171, #33342, .T. ) ;
#19964=DIRECTION ( 'NONE',  ( -1.000000000000000000, 0.000000000000000000, 0.000000000000000000 ) ) ;
#19965=EDGE_CURVE ( 'NONE', #30730, #34251, #28181, .T. ) ;
#19973=ORIENTED_EDGE ( 'NONE', *, *, #28326, .F. ) ;
#20020=DIRECTION ( 'NONE',  ( 0.000000000000000000, -1.000000000000000000, -1.040834085586082363E-14 ) ) ;
#20025=DIRECTION ( 'NONE',  ( -1.000000000000000000, 0.000000000000000000, 0.000000000000000000 ) ) ;
#20053=DIRECTION ( 'NONE',  ( -1.000000000000000000, 0.000000000000000000, 0.000000000000000000 ) ) ;
#20072=CARTESIAN_POINT ( 'NONE',  ( 8.000000000000000000, 13.55483219355744673, -11.06713717293225407 ) ) ;
#20073=EDGE_CURVE ( 'NONE', #6031, #2681, #28718, .T. ) ;
#20087=( GEOMETRIC_REPRESENTATION_CONTEXT ( 3 ) GLOBAL_UNCERTAINTY_ASSIGNED_CONTEXT ( ( #9635 ) ) GLOBAL_UNIT_ASSIGNED_CONTEXT ( ( #19540, #5193, #19028 ) ) REPRESENTATION_CONTEXT ( 'NONE', 'WORKASPACE' ) );
#20093=ORIENTED_EDGE ( 'NONE', *, *, #32436, .T. ) ;
#20095=LINE ( 'NONE', #20444, #1272 ) ;
#20100=CARTESIAN_POINT ( 'NONE',  ( 8.000000000000000000, 0.000000000000000000, 0.000000000000000000 ) ) ;
#20109=DIRECTION ( 'NONE',  ( 0.000000000000000000, -0.3090169943749350723, -0.9510565162951575280 ) ) ;
#20120=EDGE_LOOP ( 'NONE', ( #30802, #9433, #29862, #22138 ) ) ;
#20126=EDGE_LOOP ( 'NONE', ( #8685, #27770, #16568, #10111 ) ) ;
#20135=AXIS2_PLACEMENT_3D ( 'NONE', #17235, #19745, #11663 ) ;
#20156=DIRECTION ( 'NONE',  ( -1.000000000000000000, 0.000000000000000000, 0.000000000000000000 ) ) ;
#20159=ORIENTED_EDGE ( 'NONE', *, *, #19277, .F. ) ;
#20193=CARTESIAN_POINT ( 'NONE',  ( 8.000000000000000000, -13.55483219355736679, 11.06713717293235888 ) ) ;
#20239=DIRECTION ( 'NONE',  ( 1.000000000000000000, -0.000000000000000000, 0.000000000000000000 ) ) ;
#20245=EDGE_CURVE ( 'NONE', #34729, #27973, #32779, .T. ) ;
#20257=EDGE_CURVE ( 'NONE', #9536, #15604, #32126, .T. ) ;
#20260=CIRCLE ( 'NONE', #31799, 8.000000000000015987 ) ;
#20265=DIRECTION ( 'NONE',  ( -1.000000000000000000, 0.000000000000000000, 0.000000000000000000 ) ) ;
#20285=DIRECTION ( 'NONE',  ( 0.000000000000000000, 0.000000000000000000, -1.000000000000000000 ) ) ;
#20299=ORIENTED_EDGE ( 'NONE', *, *, #19565, .T. ) ;
#20301=CIRCLE ( 'NONE', #5414, 22.00000000000000000 ) ;
#20320=DIRECTION ( 'NONE',  ( 0.000000000000000000, 0.000000000000000000, 1.000000000000000000 ) ) ;
#20328=DIRECTION ( 'NONE',  ( -1.000000000000000000, 0.000000000000000000, 0.000000000000000000 ) ) ;
#20335=ORIENTED_EDGE ( 'NONE', *, *, #25330, .T. ) ;
#20336=VECTOR ( 'NONE', #4710, 1000.000000000000000 ) ;
#20346=ORIENTED_EDGE ( 'NONE', *, *, #35015, .F. ) ;
#20377=CARTESIAN_POINT ( 'NONE',  ( 8.000000000000000000, 0.000000000000000000, 0.000000000000000000 ) ) ;
#20384=ORIENTED_EDGE ( 'NONE', *, *, #2464, .F. ) ;
#20395=CARTESIAN_POINT ( 'NONE',  ( 8.000000000000000000, 16.94522934049224361, -8.128228055638670568 ) ) ;
#20396=ADVANCED_FACE ( 'NONE', ( #16615 ), #33018, .T. ) ;
#20419=ORIENTED_EDGE ( 'NONE', *, *, #21207, .T. ) ;
#20430=ADVANCED_FACE ( 'NONE', ( #30321 ), #28146, .T. ) ;
#20438=AXIS2_PLACEMENT_3D ( 'NONE', #9249, #785, #30862 ) ;
#20444=CARTESIAN_POINT ( 'NONE',  ( 8.000000000000000000, 0.9861715913090087771, -17.47118961583601049 ) ) ;
#20450=AXIS2_PLACEMENT_3D ( 'NONE', #13849, #13502, #27718 ) ;
#20462=FACE_OUTER_BOUND ( 'NONE', #8297, .T. ) ;
#20476=DIRECTION ( 'NONE',  ( 0.000000000000000000, 0.000000000000000000, -1.000000000000000000 ) ) ;
#20482=EDGE_CURVE ( 'NONE', #3103, #23381, #7186, .T. ) ;
#20483=AXIS2_PLACEMENT_3D ( 'NONE', #31073, #8918, #6399 ) ;
#20490=DIRECTION ( 'NONE',  ( -1.000000000000000000, 0.000000000000000000, 0.000000000000000000 ) ) ;
#20517=CARTESIAN_POINT ( 'NONE',  ( 8.000000000000000000, 11.06713717293239441, 13.55483219355733837 ) ) ;
#20524=VERTEX_POINT ( 'NONE', #12022 ) ;
#20531=ORIENTED_EDGE ( 'NONE', *, *, #8396, .F. ) ;
#20533=AXIS2_PLACEMENT_3D ( 'NONE', #3863, #20025, #25464 ) ;
#20557=DIRECTION ( 'NONE',  ( -1.000000000000000000, 0.000000000000000000, 0.000000000000000000 ) ) ;
#20612=ORIENTED_EDGE ( 'NONE', *, *, #20073, .T. ) ;
#20619=DIRECTION ( 'NONE',  ( 0.000000000000000000, 0.000000000000000000, 1.000000000000000000 ) ) ;
#20627=DIRECTION ( 'NONE',  ( -1.000000000000000000, 0.000000000000000000, 0.000000000000000000 ) ) ;
#20632=DIRECTION ( 'NONE',  ( 0.000000000000000000, 0.000000000000000000, 1.000000000000000000 ) ) ;
#20652=ORIENTED_EDGE ( 'NONE', *, *, #724, .F. ) ;
#20664=ADVANCED_FACE ( 'NONE', ( #25897 ), #27876, .T. ) ;
#20688=CARTESIAN_POINT ( 'NONE',  ( 8.000000000000000000, 6.071532165918824830E-15, 1.000000000000000000 ) ) ;
#20695=CARTESIAN_POINT ( 'NONE',  ( 8.000000000000000000, -15.92965478239607613, -15.17386234660400746 ) ) ;
#20709=ORIENTED_EDGE ( 'NONE', *, *, #5137, .T. ) ;
#20721=ORIENTED_EDGE ( 'NONE', *, *, #19569, .F. ) ;
#20722=ORIENTED_EDGE ( 'NONE', *, *, #30839, .T. ) ;
#20734=ORIENTED_EDGE ( 'NONE', *, *, #13664, .F. ) ;
#20738=AXIS2_PLACEMENT_3D ( 'NONE', #7578, #19087, #8106 ) ;
#20739=DIRECTION ( 'NONE',  ( 1.000000000000000000, -0.000000000000000000, -0.000000000000000000 ) ) ;
#20742=DIRECTION ( 'NONE',  ( 0.000000000000000000, 0.9510565162951544194, -0.3090169943749449533 ) ) ;
#20752=ORIENTED_EDGE ( 'NONE', *, *, #27920, .T. ) ;
#20759=STYLED_ITEM ( 'NONE', ( #24370 ), #16793 ) ;
#20760=VECTOR ( 'NONE', #22320, 1000.000000000000000 ) ;
#20804=ORIENTED_EDGE ( 'NONE', *, *, #32433, .F. ) ;
#20806=CARTESIAN_POINT ( 'NONE',  ( 8.000000000000000000, -3.384281271887680909, -18.48663108841362757 ) ) ;
#20807=FACE_OUTER_BOUND ( 'NONE', #5794, .T. ) ;
#20829=VECTOR ( 'NONE', #20557, 1000.000000000000000 ) ;
#20832=ORIENTED_EDGE ( 'NONE', *, *, #11730, .F. ) ;
#20841=CIRCLE ( 'NONE', #27209, 8.000000000000007105 ) ;
#20854=DIRECTION ( 'NONE',  ( -1.000000000000000000, 0.000000000000000000, 0.000000000000000000 ) ) ;
#20858=CARTESIAN_POINT ( 'NONE',  ( 8.000000000000000000, 0.9861715913087641949, 17.47118961583602115 ) ) ;
#20861=ORIENTED_EDGE ( 'NONE', *, *, #8721, .F. ) ;
#20884=VERTEX_POINT ( 'NONE', #15059 ) ;
#20900=EDGE_CURVE ( 'NONE', #15039, #30052, #23048, .T. ) ;
#20910=EDGE_CURVE ( 'NONE', #4881, #15404, #21350, .T. ) ;
#20929=EDGE_CURVE ( 'NONE', #4713, #7329, #35187, .T. ) ;
#20939=CARTESIAN_POINT ( 'NONE',  ( 8.000000000000000000, 5.399999999999999467, -1.000000000000003109 ) ) ;
#20944=ADVANCED_FACE ( 'NONE', ( #24091 ), #10397, .T. ) ;
#20989=EDGE_LOOP ( 'NONE', ( #6299, #1020, #34803, #26818 ) ) ;
#20990=CARTESIAN_POINT ( 'NONE',  ( 8.000000000000000000, 0.000000000000000000, 0.000000000000000000 ) ) ;
#21008=DIRECTION ( 'NONE',  ( -1.000000000000000000, 0.000000000000000000, 0.000000000000000000 ) ) ;
#21023=VECTOR ( 'NONE', #29460, 1000.000000000000000 ) ;
#21037=CARTESIAN_POINT ( 'NONE',  ( -10.00000000000000178, 0.000000000000000000, 0.000000000000000000 ) ) ;
#21043=CIRCLE ( 'NONE', #4422, 8.000000000000001776 ) ;
#21063=AXIS2_PLACEMENT_3D ( 'NONE', #32228, #7554, #26832 ) ;
#21066=VECTOR ( 'NONE', #26309, 1000.000000000000000 ) ;
#21068=ORIENTED_EDGE ( 'NONE', *, *, #12632, .F. ) ;
#21069=ORIENTED_EDGE ( 'NONE', *, *, #15490, .F. ) ;
#21081=AXIS2_PLACEMENT_3D ( 'NONE', #21147, #24057, #34315 ) ;
#21088=AXIS2_PLACEMENT_3D ( 'NONE', #34534, #18314, #26975 ) ;
#21091=CIRCLE ( 'NONE', #2734, 22.00000000000000000 ) ;
#21094=DIRECTION ( 'NONE',  ( -1.000000000000000000, 0.000000000000000000, 0.000000000000000000 ) ) ;
#21095=DIRECTION ( 'NONE',  ( -1.000000000000000000, 0.000000000000000000, 0.000000000000000000 ) ) ;
#21104=CIRCLE ( 'NONE', #24573, 8.000000000000007105 ) ;
#21112=DIRECTION ( 'NONE',  ( -1.000000000000000000, 0.000000000000000000, 0.000000000000000000 ) ) ;
#21118=SURFACE_STYLE_USAGE ( .BOTH. , #27079 ) ;
#21119=VECTOR ( 'NONE', #27462, 1000.000000000000000 ) ;
#21129=EDGE_CURVE ( 'NONE', #21342, #27071, #3364, .T. ) ;
#21144=EDGE_CURVE ( 'NONE', #26858, #4881, #24327, .T. ) ;
#21147=CARTESIAN_POINT ( 'NONE',  ( 8.000000000000000000, 8.931325931664597206, 16.53603053422209612 ) ) ;
#21171=VERTEX_POINT ( 'NONE', #6043 ) ;
#21172=ORIENTED_EDGE ( 'NONE', *, *, #19909, .F. ) ;
#21178=DIRECTION ( 'NONE',  ( -1.000000000000000000, 0.000000000000000000, 0.000000000000000000 ) ) ;
#21207=EDGE_CURVE ( 'NONE', #35010, #2129, #1310, .T. ) ;
#21212=VECTOR ( 'NONE', #1296, 1000.000000000000000 ) ;
#21213=CARTESIAN_POINT ( 'NONE',  ( 8.000000000000000000, 0.000000000000000000, 0.000000000000000000 ) ) ;
#21216=DIRECTION ( 'NONE',  ( -1.000000000000000000, 0.000000000000000000, 0.000000000000000000 ) ) ;
#21217=VERTEX_POINT ( 'NONE', #23854 ) ;
#21222=ORIENTED_EDGE ( 'NONE', *, *, #8672, .T. ) ;
#21232=ADVANCED_FACE ( 'NONE', ( #6748 ), #3892, .T. ) ;
#21288=CARTESIAN_POINT ( 'NONE',  ( 0.000000000000000000, 13.55483219355744673, -11.06713717293225407 ) ) ;
#21307=AXIS2_PLACEMENT_3D ( 'NONE', #26589, #12725, #18292 ) ;
#21314=CARTESIAN_POINT ( 'NONE',  ( 8.000000000000000000, -18.48663108841356717, -3.384281271888017084 ) ) ;
#21319=DIRECTION ( 'NONE',  ( 0.000000000000000000, -0.9510565162951564178, 0.3090169943749384585 ) ) ;
#21323=DIRECTION ( 'NONE',  ( -1.000000000000000000, 0.000000000000000000, 0.000000000000000000 ) ) ;
#21334=DIRECTION ( 'NONE',  ( 0.000000000000000000, 0.000000000000000000, 1.000000000000000000 ) ) ;
#21335=CYLINDRICAL_SURFACE ( 'NONE', #11187, 22.00000000000000000 ) ;
#21342=VERTEX_POINT ( 'NONE', #31767 ) ;
#21343=DIRECTION ( 'NONE',  ( 0.000000000000000000, 0.8090169943749448977, 0.5877852522924766898 ) ) ;
#21350=CIRCLE ( 'NONE', #27698, 22.00000000000000000 ) ;
#21368=FACE_OUTER_BOUND ( 'NONE', #14545, .T. ) ;
#21374=EDGE_CURVE ( 'NONE', #9277, #22897, #12262, .T. ) ;
#21377=ORIENTED_EDGE ( 'NONE', *, *, #21808, .T. ) ;
#21392=ADVANCED_FACE ( 'NONE', ( #18797 ), #24569, .T. ) ;
#21395=EDGE_CURVE ( 'NONE', #34729, #15733, #5936, .T. ) ;
#21403=DIRECTION ( 'NONE',  ( -1.000000000000000000, 0.000000000000000000, 0.000000000000000000 ) ) ;
#21407=DIRECTION ( 'NONE',  ( -1.000000000000000000, 0.000000000000000000, 0.000000000000000000 ) ) ;
#21438=DIRECTION ( 'NONE',  ( -1.000000000000000000, 0.000000000000000000, 0.000000000000000000 ) ) ;
#21480=DIRECTION ( 'NONE',  ( 0.000000000000000000, 0.000000000000000000, 1.000000000000000000 ) ) ;
#21481=ADVANCED_FACE ( 'NONE', ( #13235 ), #10350, .T. ) ;
#21485=DIRECTION ( 'NONE',  ( 1.000000000000000000, -0.000000000000000000, 0.000000000000000000 ) ) ;
#21489=CARTESIAN_POINT ( 'NONE',  ( 8.000000000000000000, 13.60411018104336023, -12.96676809804134400 ) ) ;
#21491=ORIENTED_EDGE ( 'NONE', *, *, #27880, .T. ) ;
#21502=DIRECTION ( 'NONE',  ( -1.000000000000000000, 0.000000000000000000, 0.000000000000000000 ) ) ;
#21520=CARTESIAN_POINT ( 'NONE',  ( -10.00000000000000178, 0.000000000000000000, 0.000000000000000000 ) ) ;
#21521=CARTESIAN_POINT ( 'NONE',  ( 8.000000000000000000, 0.000000000000000000, 0.000000000000000000 ) ) ;
#21532=VERTEX_POINT ( 'NONE', #13403 ) ;
#21534=CARTESIAN_POINT ( 'NONE',  ( 0.000000000000000000, -2.494040418455483188, 18.62763138773849292 ) ) ;
#21539=CIRCLE ( 'NONE', #859, 17.49900000000001654 ) ;
#21546=CIRCLE ( 'NONE', #26172, 8.000000000000014211 ) ;
#21563=ORIENTED_EDGE ( 'NONE', *, *, #5523, .T. ) ;
#21565=EDGE_CURVE ( 'NONE', #32655, #27460, #30796, .T. ) ;
#21566=CIRCLE ( 'NONE', #19282, 8.000000000000001776 ) ;
#21573=FACE_OUTER_BOUND ( 'NONE', #30491, .T. ) ;
#21582=ORIENTED_EDGE ( 'NONE', *, *, #33891, .F. ) ;
#21591=DIRECTION ( 'NONE',  ( 0.000000000000000000, 0.000000000000000000, 1.000000000000000000 ) ) ;
#21597=EDGE_LOOP ( 'NONE', ( #28818, #23623, #20346, #32830, #24442, #34914 ) ) ;
#21601=EDGE_CURVE ( 'NONE', #23381, #519, #35416, .T. ) ;
#21626=ADVANCED_FACE ( 'NONE', ( #11229 ), #594, .T. ) ;
#21628=VERTEX_POINT ( 'NONE', #16965 ) ;
#21634=DIRECTION ( 'NONE',  ( 0.000000000000000000, 0.000000000000000000, 1.000000000000000000 ) ) ;
#21637=CARTESIAN_POINT ( 'NONE',  ( 8.000000000000000000, -12.96676809804139197, -13.60411018104332292 ) ) ;
#21650=FILL_AREA_STYLE ('',( #35017 ) ) ;
#21668=CARTESIAN_POINT ( 'NONE',  ( 0.000000000000000000, -16.94522934049218676, 8.128228055638807348 ) ) ;
#21698=AXIS2_PLACEMENT_3D ( 'NONE', #13445, #26781, #29302 ) ;
#21725=CARTESIAN_POINT ( 'NONE',  ( 8.000000000000000000, 16.53603053422208902, -8.931325931664652273 ) ) ;
#21744=ORIENTED_EDGE ( 'NONE', *, *, #7994, .F. ) ;
#21764=VERTEX_POINT ( 'NONE', #7239 ) ;
#21772=ORIENTED_EDGE ( 'NONE', *, *, #34360, .F. ) ;
#21778=ORIENTED_EDGE ( 'NONE', *, *, #24826, .F. ) ;
#21787=FACE_OUTER_BOUND ( 'NONE', #12130, .T. ) ;
#21791=CIRCLE ( 'NONE', #28753, 8.000000000000001776 ) ;
#21808=EDGE_CURVE ( 'NONE', #180, #34183, #18742, .T. ) ;
#21811=DIRECTION ( 'NONE',  ( 0.000000000000000000, 0.000000000000000000, 1.000000000000000000 ) ) ;
#21812=CARTESIAN_POINT ( 'NONE',  ( 0.000000000000000000, -21.63912866391140710, 3.968388925834730685 ) ) ;
#21832=ORIENTED_EDGE ( 'NONE', *, *, #24081, .F. ) ;
#21855=VECTOR ( 'NONE', #5154, 1000.000000000000000 ) ;
#21868=DIRECTION ( 'NONE',  ( -1.000000000000000000, 0.000000000000000000, 0.000000000000000000 ) ) ;
#21874=CARTESIAN_POINT ( 'NONE',  ( 8.000000000000000000, -4.460989585141086344, 16.92083251265324151 ) ) ;
#21882=ORIENTED_EDGE ( 'NONE', *, *, #27913, .T. ) ;
#21915=CARTESIAN_POINT ( 'NONE',  ( 0.000000000000000000, -21.63912866391137868, -3.968388925835033554 ) ) ;
#21952=LINE ( 'NONE', #19247, #4268 ) ;
#21954=VERTEX_POINT ( 'NONE', #13197 ) ;
#21963=DIRECTION ( 'NONE',  ( 1.000000000000000000, -0.000000000000000000, -0.000000000000000000 ) ) ;
#21978=AXIS2_PLACEMENT_3D ( 'NONE', #2126, #7327, #2472 ) ;
#21985=ORIENTED_EDGE ( 'NONE', *, *, #12632, .T. ) ;
#22012=CARTESIAN_POINT ( 'NONE',  ( 0.000000000000000000, 9.471478019455140895, 14.71414642875960332 ) ) ;
#22019=CIRCLE ( 'NONE', #34704, 17.49900000000001299 ) ;
#22028=DIRECTION ( 'NONE',  ( 0.000000000000000000, 0.000000000000000000, -1.000000000000000000 ) ) ;
#22041=DIRECTION ( 'NONE',  ( -1.000000000000000000, 0.000000000000000000, 0.000000000000000000 ) ) ;
#22046=CARTESIAN_POINT ( 'NONE',  ( 8.000000000000000000, 4.460989585140964664, 16.92083251265327348 ) ) ;
#22053=EDGE_LOOP ( 'NONE', ( #15261, #34340, #27099, #24680 ) ) ;
#22059=ORIENTED_EDGE ( 'NONE', *, *, #14560, .F. ) ;
#22069=EDGE_CURVE ( 'NONE', #22471, #30312, #16393, .T. ) ;
#22091=CARTESIAN_POINT ( 'NONE',  ( 0.000000000000000000, -19.83898331853678343, -9.508666619816859011 ) ) ;
#22105=CYLINDRICAL_SURFACE ( 'NONE', #22980, 22.00000000000000000 ) ;
#22112=CARTESIAN_POINT ( 'NONE',  ( 8.000000000000000000, -18.62763138773848581, -2.494040418455559127 ) ) ;
#22114=CARTESIAN_POINT ( 'NONE',  ( 8.000000000000000000, 0.000000000000000000, 0.000000000000000000 ) ) ;
#22127=EDGE_CURVE ( 'NONE', #15307, #21532, #27400, .T. ) ;
#22138=ORIENTED_EDGE ( 'NONE', *, *, #28611, .T. ) ;
#22142=LINE ( 'NONE', #19447, #20760 ) ;
#22159=DIRECTION ( 'NONE',  ( -1.000000000000000000, 0.000000000000000000, 0.000000000000000000 ) ) ;
#22214=VECTOR ( 'NONE', #220, 1000.000000000000000 ) ;
#22221=DIRECTION ( 'NONE',  ( 0.000000000000000000, 0.000000000000000000, 1.000000000000000000 ) ) ;
#22224=EDGE_CURVE ( 'NONE', #11512, #9304, #3263, .T. ) ;
#22228=AXIS2_PLACEMENT_3D ( 'NONE', #9851, #24096, #26612 ) ;
#22252=CIRCLE ( 'NONE', #9020, 22.00000000000000000 ) ;
#22253=ADVANCED_FACE ( 'NONE', ( #9187 ), #6842, .T. ) ;
#22256=EDGE_CURVE ( 'NONE', #12175, #15307, #15310, .T. ) ;
#22257=ADVANCED_FACE ( 'NONE', ( #15106 ), #26115, .T. ) ;
#22266=DIRECTION ( 'NONE',  ( -1.000000000000000000, 0.000000000000000000, 0.000000000000000000 ) ) ;
#22267=LINE ( 'NONE', #33263, #30741 ) ;
#22292=FACE_OUTER_BOUND ( 'NONE', #23969, .T. ) ;
#22310=CIRCLE ( 'NONE', #15978, 17.49900000000001654 ) ;
#22320=DIRECTION ( 'NONE',  ( -1.000000000000000000, 0.000000000000000000, 0.000000000000000000 ) ) ;
#22330=CARTESIAN_POINT ( 'NONE',  ( 8.000000000000000000, 0.000000000000000000, 0.000000000000000000 ) ) ;
#22354=CARTESIAN_POINT ( 'NONE',  ( 8.000000000000000000, 16.92083251265325572, 4.460989585141031277 ) ) ;
#22374=ORIENTED_EDGE ( 'NONE', *, *, #27132, .T. ) ;
#22380=ORIENTED_EDGE ( 'NONE', *, *, #7347, .F. ) ;
#22389=FACE_OUTER_BOUND ( 'NONE', #26729, .T. ) ;
#22403=CARTESIAN_POINT ( 'NONE',  ( 8.000000000000000000, 8.128228055639098670, -16.94522934049206242 ) ) ;
#22409=COLOUR_RGB ( '', 0.31764706, 0.68627451, 0.89019608) ;
#22433=CARTESIAN_POINT ( 'NONE',  ( 8.000000000000000000, -12.96676809804157848, 13.60411018104313641 ) ) ;
#22453=ORIENTED_EDGE ( 'NONE', *, *, #17655, .F. ) ;
#22462=AXIS2_PLACEMENT_3D ( 'NONE', #18943, #10675, #21634 ) ;
#22464=AXIS2_PLACEMENT_3D ( 'NONE', #24155, #7936, #2020 ) ;
#22470=DIRECTION ( 'NONE',  ( -1.000000000000000000, 0.000000000000000000, -0.000000000000000000 ) ) ;
#22471=VERTEX_POINT ( 'NONE', #5403 ) ;
#22484=FACE_OUTER_BOUND ( 'NONE', #22645, .T. ) ;
#22497=EDGE_CURVE ( 'NONE', #32738, #25838, #32388, .T. ) ;
#22516=ORIENTED_EDGE ( 'NONE', *, *, #14477, .T. ) ;
#22520=DIRECTION ( 'NONE',  ( -1.000000000000000000, 0.000000000000000000, 0.000000000000000000 ) ) ;
#22551=CARTESIAN_POINT ( 'NONE',  ( 8.000000000000000000, -8.128228055638727412, -16.94522934049221519 ) ) ;
#22564=CARTESIAN_POINT ( 'NONE',  ( 0.000000000000000000, 16.94522934049215124, 8.128228055638924587 ) ) ;
#22570=ORIENTED_EDGE ( 'NONE', *, *, #3164, .F. ) ;
#22579=CARTESIAN_POINT ( 'NONE',  ( 8.000000000000000000, 5.400000000000021672, 1.000000000000001776 ) ) ;
#22586=CARTESIAN_POINT ( 'NONE',  ( 4.000000000000003553, 15.17386234660384581, 15.92965478239621824 ) ) ;
#22594=DIRECTION ( 'NONE',  ( -1.000000000000000000, 0.000000000000000000, 0.000000000000000000 ) ) ;
#22613=FACE_OUTER_BOUND ( 'NONE', #9584, .T. ) ;
#22635=DIRECTION ( 'NONE',  ( -1.000000000000000000, 0.000000000000000000, 0.000000000000000000 ) ) ;
#22638=DIRECTION ( 'NONE',  ( 0.000000000000000000, 0.000000000000000000, 1.000000000000000000 ) ) ;
#22644=AXIS2_PLACEMENT_3D ( 'NONE', #14274, #3322, #245 ) ;
#22645=EDGE_LOOP ( 'NONE', ( #17091, #12516, #7470, #8468 ) ) ;
#22687=AXIS2_PLACEMENT_3D ( 'NONE', #15249, #21008, #7353 ) ;
#22700=CARTESIAN_POINT ( 'NONE',  ( 0.000000000000000000, -16.92083251265322019, -4.460989585141143188 ) ) ;
#22729=EDGE_CURVE ( 'NONE', #30389, #25690, #2465, .T. ) ;
#22741=EDGE_CURVE ( 'NONE', #34512, #21171, #249, .T. ) ;
#22748=CARTESIAN_POINT ( 'NONE',  ( 8.000000000000000000, 18.48663108841359559, -3.384281271887881637 ) ) ;
#22775=AXIS2_PLACEMENT_3D ( 'NONE', #16275, #32153, #29994 ) ;
#22778=CYLINDRICAL_SURFACE ( 'NONE', #14175, 17.49900000000000233 ) ;
#22790=CIRCLE ( 'NONE', #25694, 8.000000000000008882 ) ;
#22797=DIRECTION ( 'NONE',  ( 0.000000000000000000, 0.000000000000000000, -1.000000000000000000 ) ) ;
#22801=FACE_OUTER_BOUND ( 'NONE', #31932, .T. ) ;
#22803=ORIENTED_EDGE ( 'NONE', *, *, #23949, .T. ) ;
#22808=CARTESIAN_POINT ( 'NONE',  ( 8.000000000000000000, -0.9861715913088822116, 17.47118961583599273 ) ) ;
#22821=CARTESIAN_POINT ( 'NONE',  ( 8.000000000000000000, 0.000000000000000000, 0.000000000000000000 ) ) ;
#22835=ORIENTED_EDGE ( 'NONE', *, *, #34122, .T. ) ;
#22839=ORIENTED_EDGE ( 'NONE', *, *, #25959, .F. ) ;
#22845=AXIS2_PLACEMENT_3D ( 'NONE', #1838, #12813, #18557 ) ;
#22857=EDGE_CURVE ( 'NONE', #9043, #34436, #27744, .T. ) ;
#22863=VECTOR ( 'NONE', #26709, 1000.000000000000000 ) ;
#22874=CIRCLE ( 'NONE', #15958, 17.49900000000000944 ) ;
#22897=VERTEX_POINT ( 'NONE', #20193 ) ;
#22911=CYLINDRICAL_SURFACE ( 'NONE', #7724, 17.49900000000000233 ) ;
#22922=FACE_BOUND ( 'NONE', #21597, .T. ) ;
#22944=CIRCLE ( 'NONE', #7434, 22.00000000000000000 ) ;
#22958=FACE_OUTER_BOUND ( 'NONE', #9370, .T. ) ;
#22962=VERTEX_POINT ( 'NONE', #4038 ) ;
#22973=EDGE_CURVE ( 'NONE', #15039, #27914, #17380, .T. ) ;
#22974=AXIS2_PLACEMENT_3D ( 'NONE', #27180, #35114, #15989 ) ;
#22979=CARTESIAN_POINT ( 'NONE',  ( 8.000000000000000000, 4.898587196589412829E-16, -4.000000000000000000 ) ) ;
#22980=AXIS2_PLACEMENT_3D ( 'NONE', #14347, #27871, #4804 ) ;
#22994=AXIS2_PLACEMENT_3D ( 'NONE', #18792, #18615, #32666 ) ;
#22995=DIRECTION ( 'NONE',  ( -1.000000000000000000, 0.000000000000000000, 0.000000000000000000 ) ) ;
#23023=DIRECTION ( 'NONE',  ( 0.000000000000000000, 0.000000000000000000, 1.000000000000000000 ) ) ;
#23030=AXIS2_PLACEMENT_3D ( 'NONE', #9604, #26715, #15161 ) ;
#23041=DIRECTION ( 'NONE',  ( 0.000000000000000000, -0.8090169943749405679, -0.5877852522924826850 ) ) ;
#23042=VERTEX_POINT ( 'NONE', #9950 ) ;
#23048=CIRCLE ( 'NONE', #19044, 8.000000000000001776 ) ;
#23056=VECTOR ( 'NONE', #25244, 1000.000000000000000 ) ;
#23058=VERTEX_POINT ( 'NONE', #32099 ) ;
#23065=EDGE_LOOP ( 'NONE', ( #33630, #25908, #33032, #32139 ) ) ;
#23066=EDGE_CURVE ( 'NONE', #29327, #25342, #17973, .T. ) ;
#23100=CARTESIAN_POINT ( 'NONE',  ( 8.000000000000000000, -16.92083251265322374, -4.460989585141144076 ) ) ;
#23114=VERTEX_POINT ( 'NONE', #4923 ) ;
#23115=ORIENTED_EDGE ( 'NONE', *, *, #6391, .T. ) ;
#23128=DIRECTION ( 'NONE',  ( 1.000000000000000000, -0.000000000000000000, -0.000000000000000000 ) ) ;
#23136=CARTESIAN_POINT ( 'NONE',  ( 0.000000000000000000, -15.17386234660370370, -15.92965478239635679 ) ) ;
#23137=DIRECTION ( 'NONE',  ( -1.000000000000000000, 0.000000000000000000, 0.000000000000000000 ) ) ;
#23143=EDGE_CURVE ( 'NONE', #2115, #23114, #20841, .T. ) ;
#23145=DIRECTION ( 'NONE',  ( 0.000000000000000000, 0.000000000000000000, 1.000000000000000000 ) ) ;
#23152=ORIENTED_EDGE ( 'NONE', *, *, #29343, .F. ) ;
#23161=VECTOR ( 'NONE', #34752, 1000.000000000000000 ) ;
#23182=DIRECTION ( 'NONE',  ( -1.000000000000000000, 0.000000000000000000, 0.000000000000000000 ) ) ;
#23197=CARTESIAN_POINT ( 'NONE',  ( 8.000000000000000000, -14.71414642875948608, -9.471478019455300768 ) ) ;
#23201=VERTEX_POINT ( 'NONE', #21812 ) ;
#23202=EDGE_CURVE ( 'NONE', #27071, #2828, #10513, .T. ) ;
#23212=AXIS2_PLACEMENT_3D ( 'NONE', #35033, #21485, #7285 ) ;
#23226=DIRECTION ( 'NONE',  ( 0.000000000000000000, 0.000000000000000000, 1.000000000000000000 ) ) ;
#23237=AXIS2_PLACEMENT_3D ( 'NONE', #34759, #20328, #10082 ) ;
#23266=CARTESIAN_POINT ( 'NONE',  ( 8.000000000000000000, 6.336799421340039373, -16.31134495048478428 ) ) ;
#23295=CYLINDRICAL_SURFACE ( 'NONE', #27170, 17.49900000000000233 ) ;
#23299=LINE ( 'NONE', #2034, #10250 ) ;
#23313=DIRECTION ( 'NONE',  ( -1.000000000000000000, 0.000000000000000000, 0.000000000000000000 ) ) ;
#23342=AXIS2_PLACEMENT_3D ( 'NONE', #34681, #25689, #29097 ) ;
#23346=VERTEX_POINT ( 'NONE', #32213 ) ;
#23349=VECTOR ( 'NONE', #13806, 1000.000000000000000 ) ;
#23361=AXIS2_PLACEMENT_3D ( 'NONE', #32049, #29182, #23766 ) ;
#23381=VERTEX_POINT ( 'NONE', #31506 ) ;
#23391=ORIENTED_EDGE ( 'NONE', *, *, #31320, .T. ) ;
#23394=CIRCLE ( 'NONE', #8459, 8.000000000000003553 ) ;
#23422=ORIENTED_EDGE ( 'NONE', *, *, #33233, .F. ) ;
#23425=CARTESIAN_POINT ( 'NONE',  ( 0.000000000000000000, 0.000000000000000000, 4.000000000000000000 ) ) ;
#23432=DIRECTION ( 'NONE',  ( 1.000000000000000000, -0.000000000000000000, -0.000000000000000000 ) ) ;
#23435=ORIENTED_EDGE ( 'NONE', *, *, #27132, .F. ) ;
#23447=CARTESIAN_POINT ( 'NONE',  ( 0.000000000000000000, -8.128228055638727412, -16.94522934049221519 ) ) ;
#23454=DIRECTION ( 'NONE',  ( 1.000000000000000000, -0.000000000000000000, -0.000000000000000000 ) ) ;
#23460=ORIENTED_EDGE ( 'NONE', *, *, #24826, .T. ) ;
#23464=CARTESIAN_POINT ( 'NONE',  ( 0.000000000000000000, -16.53603053422202862, -8.931325931664767737 ) ) ;
#23465=ORIENTED_EDGE ( 'NONE', *, *, #9904, .T. ) ;
#23479=ORIENTED_EDGE ( 'NONE', *, *, #11474, .F. ) ;
#23488=CARTESIAN_POINT ( 'NONE',  ( 0.000000000000000000, 0.000000000000000000, 0.000000000000000000 ) ) ;
#23489=EDGE_CURVE ( 'NONE', #27865, #25795, #4800, .T. ) ;
#23502=CYLINDRICAL_SURFACE ( 'NONE', #24553, 8.000000000000000000 ) ;
#23515=ORIENTED_EDGE ( 'NONE', *, *, #22224, .T. ) ;
#23522=CIRCLE ( 'NONE', #1120, 17.49900000000001299 ) ;
#23536=FACE_OUTER_BOUND ( 'NONE', #23831, .T. ) ;
#23540=DIRECTION ( 'NONE',  ( -1.000000000000000000, 0.000000000000000000, 0.000000000000000000 ) ) ;
#23545=ORIENTED_EDGE ( 'NONE', *, *, #32426, .T. ) ;
#23552=CIRCLE ( 'NONE', #22974, 8.000000000000007105 ) ;
#23574=DIRECTION ( 'NONE',  ( -1.000000000000000000, 0.000000000000000000, 0.000000000000000000 ) ) ;
#23580=CARTESIAN_POINT ( 'NONE',  ( 0.000000000000000000, -14.71414642875948608, -9.471478019455300768 ) ) ;
#23588=CARTESIAN_POINT ( 'NONE',  ( 0.000000000000000000, 0.000000000000000000, 0.000000000000000000 ) ) ;
#23592=VERTEX_POINT ( 'NONE', #3741 ) ;
#23613=ORIENTED_EDGE ( 'NONE', *, *, #7994, .T. ) ;
#23623=ORIENTED_EDGE ( 'NONE', *, *, #22069, .F. ) ;
#23632=AXIS2_PLACEMENT_3D ( 'NONE', #11655, #26606, #4118 ) ;
#23638=ORIENTED_EDGE ( 'NONE', *, *, #23143, .F. ) ;
#23647=CARTESIAN_POINT ( 'NONE',  ( 0.000000000000000000, 3.968388925835109049, -21.63912866391136447 ) ) ;
#23663=VERTEX_POINT ( 'NONE', #33989 ) ;
#23682=DIRECTION ( 'NONE',  ( -1.000000000000000000, 0.000000000000000000, 0.000000000000000000 ) ) ;
#23686=ORIENTED_EDGE ( 'NONE', *, *, #32768, .F. ) ;
#23687=AXIS2_PLACEMENT_3D ( 'NONE', #7756, #7413, #18739 ) ;
#23696=ORIENTED_EDGE ( 'NONE', *, *, #12766, .T. ) ;
#23717=CARTESIAN_POINT ( 'NONE',  ( 50.00005079999999680, 0.000000000000000000, 0.000000000000000000 ) ) ;
#23735=ORIENTED_EDGE ( 'NONE', *, *, #3783, .T. ) ;
#23754=CARTESIAN_POINT ( 'NONE',  ( 8.000000000000000000, 0.9861715913090087771, -17.47118961583601049 ) ) ;
#23757=EDGE_CURVE ( 'NONE', #28798, #26858, #22019, .T. ) ;
#23761=AXIS2_PLACEMENT_3D ( 'NONE', #4121, #4295, #6266 ) ;
#23766=DIRECTION ( 'NONE',  ( 0.000000000000000000, 0.000000000000000000, 1.000000000000000000 ) ) ;
#23772=EDGE_CURVE ( 'NONE', #18771, #20524, #31224, .T. ) ;
#23776=ORIENTED_EDGE ( 'NONE', *, *, #28388, .T. ) ;
#23780=EDGE_LOOP ( 'NONE', ( #5058, #21772, #13510, #25833 ) ) ;
#23829=CARTESIAN_POINT ( 'NONE',  ( 8.000000000000000000, -13.55483219355736679, 11.06713717293235888 ) ) ;
#23831=EDGE_LOOP ( 'NONE', ( #30853, #4516, #23515, #29063 ) ) ;
#23843=AXIS2_PLACEMENT_3D ( 'NONE', #24311, #7910, #29891 ) ;
#23845=EDGE_CURVE ( 'NONE', #30950, #21764, #6518, .T. ) ;
#23854=CARTESIAN_POINT ( 'NONE',  ( 0.000000000000000000, -9.471478019455027209, -14.71414642875966017 ) ) ;
#23855=EDGE_CURVE ( 'NONE', #12176, #272, #20301, .T. ) ;
#23879=VECTOR ( 'NONE', #24196, 1000.000000000000000 ) ;
#23897=DIRECTION ( 'NONE',  ( -1.000000000000000000, 0.000000000000000000, 0.000000000000000000 ) ) ;
#23904=DIRECTION ( 'NONE',  ( -1.000000000000000000, 0.000000000000000000, 0.000000000000000000 ) ) ;
#23909=VECTOR ( 'NONE', #24310, 1000.000000000000000 ) ;
#23919=EDGE_LOOP ( 'NONE', ( #2550, #34285, #7656, #29424 ) ) ;
#23922=CIRCLE ( 'NONE', #8371, 17.49900000000000233 ) ;
#23926=ORIENTED_EDGE ( 'NONE', *, *, #18229, .F. ) ;
#23946=CARTESIAN_POINT ( 'NONE',  ( 4.000000000000003553, -2.912696353505664248, -21.80633394113455736 ) ) ;
#23949=EDGE_CURVE ( 'NONE', #17877, #23592, #7110, .T. ) ;
#23951=DIRECTION ( 'NONE',  ( 0.000000000000000000, 0.000000000000000000, 1.000000000000000000 ) ) ;
#23966=ORIENTED_EDGE ( 'NONE', *, *, #2072, .F. ) ;
#23968=DIRECTION ( 'NONE',  ( -1.000000000000000000, 0.000000000000000000, 0.000000000000000000 ) ) ;
#23969=EDGE_LOOP ( 'NONE', ( #23735, #25577, #21491, #1082 ) ) ;
#23979=CARTESIAN_POINT ( 'NONE',  ( 0.000000000000000000, 18.48663108841359559, -3.384281271887881637 ) ) ;
#23984=ADVANCED_FACE ( 'NONE', ( #23536 ), #26244, .F. ) ;
#23987=DIRECTION ( 'NONE',  ( 1.000000000000000000, -0.000000000000000000, 0.000000000000000000 ) ) ;
#23994=FACE_OUTER_BOUND ( 'NONE', #27729, .T. ) ;
#24006=FACE_OUTER_BOUND ( 'NONE', #14584, .T. ) ;
#24007=CARTESIAN_POINT ( 'NONE',  ( 8.000000000000000000, -13.60411018104308667, -12.96676809804163000 ) ) ;
#24015=CARTESIAN_POINT ( 'NONE',  ( 8.000000000000000000, -21.80633394113452184, 2.912696353505742852 ) ) ;
#24043=ADVANCED_FACE ( 'NONE', ( #31999 ), #6795, .F. ) ;
#24049=DIRECTION ( 'NONE',  ( -1.000000000000000000, 0.000000000000000000, 0.000000000000000000 ) ) ;
#24053=CYLINDRICAL_SURFACE ( 'NONE', #26627, 8.000000000000001776 ) ;
#24057=DIRECTION ( 'NONE',  ( -1.000000000000000000, 0.000000000000000000, 0.000000000000000000 ) ) ;
#24077=CIRCLE ( 'NONE', #13148, 8.000000000000008882 ) ;
#24078=ORIENTED_EDGE ( 'NONE', *, *, #12388, .F. ) ;
#24080=DIRECTION ( 'NONE',  ( -1.000000000000000000, 0.000000000000000000, 0.000000000000000000 ) ) ;
#24081=EDGE_CURVE ( 'NONE', #5415, #9277, #5960, .T. ) ;
#24086=LINE ( 'NONE', #32169, #8730 ) ;
#24091=FACE_OUTER_BOUND ( 'NONE', #17523, .T. ) ;
#24096=DIRECTION ( 'NONE',  ( -1.000000000000000000, 0.000000000000000000, 0.000000000000000000 ) ) ;
#24102=ORIENTED_EDGE ( 'NONE', *, *, #12850, .T. ) ;
#24106=ADVANCED_FACE ( 'NONE', ( #25272 ), #73, .T. ) ;
#24113=CIRCLE ( 'NONE', #14311, 8.000000000000001776 ) ;
#24118=ORIENTED_EDGE ( 'NONE', *, *, #12102, .F. ) ;
#24131=DIRECTION ( 'NONE',  ( -1.000000000000000000, 0.000000000000000000, 0.000000000000000000 ) ) ;
#24132=LINE ( 'NONE', #10447, #16675 ) ;
#24146=CYLINDRICAL_SURFACE ( 'NONE', #34716, 17.49900000000000233 ) ;
#24155=CARTESIAN_POINT ( 'NONE',  ( 50.00005079999999680, 6.071532165918824830E-15, 1.000000000000000000 ) ) ;
#24162=VERTEX_POINT ( 'NONE', #13932 ) ;
#24189=ORIENTED_EDGE ( 'NONE', *, *, #19318, .T. ) ;
#24196=DIRECTION ( 'NONE',  ( 1.000000000000000000, -0.000000000000000000, -0.000000000000000000 ) ) ;
#24199=EDGE_CURVE ( 'NONE', #11194, #9658, #33005, .T. ) ;
#24227=ADVANCED_FACE ( 'NONE', ( #19661 ), #6006, .T. ) ;
#24236=FACE_OUTER_BOUND ( 'NONE', #28228, .T. ) ;
#24266=DIRECTION ( 'NONE',  ( 0.000000000000000000, 0.3090169943749477288, -0.9510565162951534202 ) ) ;
#24278=VERTEX_POINT ( 'NONE', #1490 ) ;
#24279=ORIENTED_EDGE ( 'NONE', *, *, #3862, .T. ) ;
#24284=ADVANCED_FACE ( 'NONE', ( #9235 ), #22911, .T. ) ;
#24292=ORIENTED_EDGE ( 'NONE', *, *, #14477, .F. ) ;
#24307=FACE_OUTER_BOUND ( 'NONE', #10599, .T. ) ;
#24310=DIRECTION ( 'NONE',  ( 0.000000000000000000, -1.000000000000000000, 0.000000000000000000 ) ) ;
#24311=CARTESIAN_POINT ( 'NONE',  ( 8.000000000000000000, -18.48663108841356717, -3.384281271888017084 ) ) ;
#24314=VERTEX_POINT ( 'NONE', #772 ) ;
#24323=CYLINDRICAL_SURFACE ( 'NONE', #24380, 8.000000000000001776 ) ;
#24327=CIRCLE ( 'NONE', #19688, 8.000000000000005329 ) ;
#24335=EDGE_LOOP ( 'NONE', ( #18341, #31188, #8548, #16711 ) ) ;
#24352=ORIENTED_EDGE ( 'NONE', *, *, #22127, .T. ) ;
#24364=ORIENTED_EDGE ( 'NONE', *, *, #11859, .T. ) ;
#24370=PRESENTATION_STYLE_ASSIGNMENT (( #21118 ) ) ;
#24378=DIRECTION ( 'NONE',  ( -1.000000000000000000, 0.000000000000000000, 0.000000000000000000 ) ) ;
#24379=APPLICATION_CONTEXT ( 'automotive_design' ) ;
#24380=AXIS2_PLACEMENT_3D ( 'NONE', #24496, #35314, #21591 ) ;
#24398=ORIENTED_EDGE ( 'NONE', *, *, #16902, .F. ) ;
#24404=DIRECTION ( 'NONE',  ( 1.000000000000000000, -0.000000000000000000, 0.000000000000000000 ) ) ;
#24407=AXIS2_PLACEMENT_3D ( 'NONE', #28428, #3773, #14729 ) ;
#24420=ORIENTED_EDGE ( 'NONE', *, *, #29552, .F. ) ;
#24427=DIRECTION ( 'NONE',  ( -1.000000000000000000, 0.000000000000000000, 0.000000000000000000 ) ) ;
#24442=ORIENTED_EDGE ( 'NONE', *, *, #32103, .F. ) ;
#24447=ORIENTED_EDGE ( 'NONE', *, *, #19277, .T. ) ;
#24459=CIRCLE ( 'NONE', #30797, 8.000000000000000000 ) ;
#24465=ADVANCED_FACE ( 'NONE', ( #10125 ), #29403, .T. ) ;
#24472=AXIS2_PLACEMENT_3D ( 'NONE', #25411, #28816, #26117 ) ;
#24488=EDGE_LOOP ( 'NONE', ( #11968, #35011, #28426, #16329 ) ) ;
#24496=CARTESIAN_POINT ( 'NONE',  ( 8.000000000000000000, 8.931325931664870765, -16.53603053422199665 ) ) ;
#24503=ORIENTED_EDGE ( 'NONE', *, *, #14560, .T. ) ;
#24515=VERTEX_POINT ( 'NONE', #18581 ) ;
#24516=EDGE_CURVE ( 'NONE', #17129, #1113, #21539, .T. ) ;
#24525=CIRCLE ( 'NONE', #25080, 8.000000000000008882 ) ;
#24542=AXIS2_PLACEMENT_3D ( 'NONE', #30941, #6273, #25733 ) ;
#24552=VECTOR ( 'NONE', #23432, 1000.000000000000000 ) ;
#24553=AXIS2_PLACEMENT_3D ( 'NONE', #7295, #35044, #18084 ) ;
#24556=VERTEX_POINT ( 'NONE', #8124 ) ;
#24559=DIRECTION ( 'NONE',  ( -1.000000000000000000, 0.000000000000000000, 0.000000000000000000 ) ) ;
#24569=CYLINDRICAL_SURFACE ( 'NONE', #26069, 8.000000000000001776 ) ;
#24573=AXIS2_PLACEMENT_3D ( 'NONE', #18819, #4803, #5331 ) ;
#24581=VERTEX_POINT ( 'NONE', #16395 ) ;
#24587=DIRECTION ( 'NONE',  ( -1.000000000000000000, 0.000000000000000000, 0.000000000000000000 ) ) ;
#24588=EDGE_LOOP ( 'NONE', ( #20384, #6645, #20652, #26004, #2936, #16598 ) ) ;
#24600=EDGE_LOOP ( 'NONE', ( #20722, #27828, #9261, #29481 ) ) ;
#24604=EDGE_CURVE ( 'NONE', #29018, #24581, #1437, .T. ) ;
#24607=EDGE_LOOP ( 'NONE', ( #5162, #12853, #8802, #26591 ) ) ;
#24610=CARTESIAN_POINT ( 'NONE',  ( 8.000000000000000000, 18.62763138773855687, 2.494040418455418351 ) ) ;
#24617=AXIS2_PLACEMENT_3D ( 'NONE', #30603, #3432, #5938 ) ;
#24626=LINE ( 'NONE', #2672, #847 ) ;
#24657=FACE_OUTER_BOUND ( 'NONE', #7919, .T. ) ;
#24661=DIRECTION ( 'NONE',  ( -1.000000000000000000, 0.000000000000000000, 0.000000000000000000 ) ) ;
#24672=FACE_OUTER_BOUND ( 'NONE', #25617, .T. ) ;
#24680=ORIENTED_EDGE ( 'NONE', *, *, #32625, .T. ) ;
#24685=CARTESIAN_POINT ( 'NONE',  ( 8.000000000000000000, 18.48663108841359559, -3.384281271887881637 ) ) ;
#24696=CARTESIAN_POINT ( 'NONE',  ( 8.000000000000000000, -16.92083251265328769, 4.460989585140905156 ) ) ;
#24711=ORIENTED_EDGE ( 'NONE', *, *, #26844, .T. ) ;
#24731=CARTESIAN_POINT ( 'NONE',  ( 8.000000000000000000, 3.872983346207429900, 1.000000000000003109 ) ) ;
#24735=CYLINDRICAL_SURFACE ( 'NONE', #33837, 8.000000000000000000 ) ;
#24745=DIRECTION ( 'NONE',  ( 0.000000000000000000, 0.000000000000000000, 1.000000000000000000 ) ) ;
#24754=DIRECTION ( 'NONE',  ( -1.000000000000000000, 0.000000000000000000, 0.000000000000000000 ) ) ;
#24761=LINE ( 'NONE', #30343, #6924 ) ;
#24765=DIRECTION ( 'NONE',  ( -1.000000000000000000, 0.000000000000000000, 0.000000000000000000 ) ) ;
#24770=EDGE_LOOP ( 'NONE', ( #13642, #18140, #20093, #6809 ) ) ;
#24775=AXIS2_PLACEMENT_3D ( 'NONE', #29490, #4829, #13117 ) ;
#24781=DIRECTION ( 'NONE',  ( -1.000000000000000000, 0.000000000000000000, 0.000000000000000000 ) ) ;
#24785=FACE_OUTER_BOUND ( 'NONE', #9552, .T. ) ;
#24787=CARTESIAN_POINT ( 'NONE',  ( 0.000000000000000000, 13.60411018104336023, -12.96676809804134400 ) ) ;
#24797=SURFACE_STYLE_USAGE ( .BOTH. , #29852 ) ;
#24798=VERTEX_POINT ( 'NONE', #34410 ) ;
#24809=CARTESIAN_POINT ( 'NONE',  ( 8.000000000000000000, 18.48663108841356717, 3.384281271888136988 ) ) ;
#24816=ORIENTED_EDGE ( 'NONE', *, *, #34394, .T. ) ;
#24826=EDGE_CURVE ( 'NONE', #2129, #8092, #16964, .T. ) ;
#24832=CARTESIAN_POINT ( 'NONE',  ( 8.000000000000000000, -13.60411018104308667, -12.96676809804163000 ) ) ;
#24838=CARTESIAN_POINT ( 'NONE',  ( 0.000000000000000000, -9.471478019455243924, 14.71414642875952161 ) ) ;
#24845=CARTESIAN_POINT ( 'NONE',  ( 4.000000000000003553, 2.912696353505820124, 21.80633394113451473 ) ) ;
#24857=LINE ( 'NONE', #8281, #34570 ) ;
#24865=EDGE_CURVE ( 'NONE', #4346, #11860, #35402, .T. ) ;
#24880=EDGE_CURVE ( 'NONE', #15127, #11959, #9727, .T. ) ;
#24887=ORIENTED_EDGE ( 'NONE', *, *, #1789, .F. ) ;
#24900=ADVANCED_FACE ( 'NONE', ( #14404 ), #14577, .T. ) ;
#24914=EDGE_CURVE ( 'NONE', #32151, #30389, #15467, .T. ) ;
#24922=ORIENTED_EDGE ( 'NONE', *, *, #9369, .F. ) ;
#24925=CARTESIAN_POINT ( 'NONE',  ( 3.999999999999996447, -3.968388925834655190, -21.63912866391144618 ) ) ;
#24938=ORIENTED_EDGE ( 'NONE', *, *, #2261, .F. ) ;
#24942=LINE ( 'NONE', #21874, #29508 ) ;
#24955=LINE ( 'NONE', #30361, #11049 ) ;
#24972=PRESENTATION_STYLE_ASSIGNMENT (( #24797 ) ) ;
#24980=DIRECTION ( 'NONE',  ( 0.000000000000000000, 0.3090169943749412895, 0.9510565162951555296 ) ) ;
#25004=DIRECTION ( 'NONE',  ( -1.000000000000000000, 0.000000000000000000, 0.000000000000000000 ) ) ;
#25015=DIRECTION ( 'NONE',  ( -1.000000000000000000, 0.000000000000000000, 0.000000000000000000 ) ) ;
#25019=AXIS2_PLACEMENT_3D ( 'NONE', #16540, #13679, #14015 ) ;
#25021=AXIS2_PLACEMENT_3D ( 'NONE', #31603, #31074, #28909 ) ;
#25026=DIRECTION ( 'NONE',  ( 0.000000000000000000, 0.000000000000000000, 1.000000000000000000 ) ) ;
#25036=VERTEX_POINT ( 'NONE', #34952 ) ;
#25044=DIRECTION ( 'NONE',  ( 0.000000000000000000, 0.5877852522924738032, -0.8090169943749468962 ) ) ;
#25052=ORIENTED_EDGE ( 'NONE', *, *, #34427, .F. ) ;
#25068=EDGE_LOOP ( 'NONE', ( #6671, #13566, #25591, #8860 ) ) ;
#25072=CARTESIAN_POINT ( 'NONE',  ( 8.000000000000000000, 21.63912866391145329, -3.968388925834584136 ) ) ;
#25080=AXIS2_PLACEMENT_3D ( 'NONE', #31393, #9964, #28339 ) ;
#25082=EDGE_CURVE ( 'NONE', #24515, #9009, #10096, .T. ) ;
#25089=DIRECTION ( 'NONE',  ( -1.000000000000000000, 0.000000000000000000, 0.000000000000000000 ) ) ;
#25097=EDGE_CURVE ( 'NONE', #16380, #18803, #21566, .T. ) ;
#25168=EDGE_CURVE ( 'NONE', #8935, #2111, #1488, .T. ) ;
#25192=CARTESIAN_POINT ( 'NONE',  ( 4.000000000000003553, 21.63912866391140710, 3.968388925834887893 ) ) ;
#25196=DIRECTION ( 'NONE',  ( 1.000000000000000000, -0.000000000000000000, 0.000000000000000000 ) ) ;
#25203=CARTESIAN_POINT ( 'NONE',  ( 8.000000000000000000, -16.31134495048480559, -6.336799421339987859 ) ) ;
#25237=ORIENTED_EDGE ( 'NONE', *, *, #2986, .T. ) ;
#25241=DIRECTION ( 'NONE',  ( 0.000000000000000000, 0.000000000000000000, 1.000000000000000000 ) ) ;
#25242=EDGE_LOOP ( 'NONE', ( #24922, #30383, #35152, #8848 ) ) ;
#25244=DIRECTION ( 'NONE',  ( -1.000000000000000000, 0.000000000000000000, 0.000000000000000000 ) ) ;
#25272=FACE_OUTER_BOUND ( 'NONE', #20989, .T. ) ;
#25274=EDGE_CURVE ( 'NONE', #16647, #31433, #25372, .T. ) ;
#25277=DIRECTION ( 'NONE',  ( 0.000000000000000000, 0.000000000000000000, 1.000000000000000000 ) ) ;
#25310=DIRECTION ( 'NONE',  ( -1.000000000000000000, 0.000000000000000000, 0.000000000000000000 ) ) ;
#25330=EDGE_CURVE ( 'NONE', #16289, #4447, #17580, .T. ) ;
#25342=VERTEX_POINT ( 'NONE', #17413 ) ;
#25344=DIRECTION ( 'NONE',  ( -1.000000000000000000, 0.000000000000000000, 0.000000000000000000 ) ) ;
#25364=CYLINDRICAL_SURFACE ( 'NONE', #16287, 8.000000000000001776 ) ;
#25372=LINE ( 'NONE', #31477, #32526 ) ;
#25384=CARTESIAN_POINT ( 'NONE',  ( 0.000000000000000000, 17.47118961583601759, 0.9861715913088272556 ) ) ;
#25388=ORIENTED_EDGE ( 'NONE', *, *, #9369, .T. ) ;
#25391=( GEOMETRIC_REPRESENTATION_CONTEXT ( 3 ) GLOBAL_UNCERTAINTY_ASSIGNED_CONTEXT ( ( #34081 ) ) GLOBAL_UNIT_ASSIGNED_CONTEXT ( ( #32650, #27437, #2785 ) ) REPRESENTATION_CONTEXT ( 'NONE', 'WORKASPACE' ) );
#25394=DIRECTION ( 'NONE',  ( 0.000000000000000000, 0.000000000000000000, -1.000000000000000000 ) ) ;
#25411=CARTESIAN_POINT ( 'NONE',  ( 8.000000000000000000, 16.53603053422211389, 8.931325931664652273 ) ) ;
#25414=ORIENTED_EDGE ( 'NONE', *, *, #5758, .T. ) ;
#25421=FACE_OUTER_BOUND ( 'NONE', #6326, .T. ) ;
#25428=ORIENTED_EDGE ( 'NONE', *, *, #35066, .F. ) ;
#25436=DIRECTION ( 'NONE',  ( -1.000000000000000000, 0.000000000000000000, 0.000000000000000000 ) ) ;
#25464=DIRECTION ( 'NONE',  ( 0.000000000000000000, 0.000000000000000000, 1.000000000000000000 ) ) ;
#25486=CIRCLE ( 'NONE', #14534, 8.000000000000005329 ) ;
#25516=AXIS2_PLACEMENT_3D ( 'NONE', #7081, #21112, #34821 ) ;
#25517=ORIENTED_EDGE ( 'NONE', *, *, #15444, .F. ) ;
#25527=CARTESIAN_POINT ( 'NONE',  ( 0.000000000000000000, 11.06713717293261467, -13.55483219355716606 ) ) ;
#25548=ORIENTED_EDGE ( 'NONE', *, *, #10815, .T. ) ;
#25573=VERTEX_POINT ( 'NONE', #34903 ) ;
#25577=ORIENTED_EDGE ( 'NONE', *, *, #28455, .T. ) ;
#25586=CARTESIAN_POINT ( 'NONE',  ( 8.000000000000000000, 0.000000000000000000, 0.000000000000000000 ) ) ;
#25591=ORIENTED_EDGE ( 'NONE', *, *, #4602, .F. ) ;
#25593=VERTEX_POINT ( 'NONE', #7680 ) ;
#25601=CIRCLE ( 'NONE', #14648, 22.00000000000000000 ) ;
#25615=LINE ( 'NONE', #27950, #31649 ) ;
#25617=EDGE_LOOP ( 'NONE', ( #33354, #9699, #13358, #24279 ) ) ;
#25632=CARTESIAN_POINT ( 'NONE',  ( 8.000000000000000000, 0.000000000000000000, 0.000000000000000000 ) ) ;
#25641=CARTESIAN_POINT ( 'NONE',  ( 8.000000000000000000, -4.460989585140847424, -16.92083251265332322 ) ) ;
#25666=DIRECTION ( 'NONE',  ( 0.000000000000000000, 0.5877852522924681411, 0.8090169943749510040 ) ) ;
#25689=DIRECTION ( 'NONE',  ( -1.000000000000000000, 0.000000000000000000, 0.000000000000000000 ) ) ;
#25690=VERTEX_POINT ( 'NONE', #19371 ) ;
#25692=ORIENTED_EDGE ( 'NONE', *, *, #23772, .T. ) ;
#25694=AXIS2_PLACEMENT_3D ( 'NONE', #19472, #30470, #3109 ) ;
#25710=VERTEX_POINT ( 'NONE', #33072 ) ;
#25726=AXIS2_PLACEMENT_3D ( 'NONE', #12816, #16019, #10101 ) ;
#25733=DIRECTION ( 'NONE',  ( 0.000000000000000000, -6.938893903907228378E-15, 1.000000000000000000 ) ) ;
#25736=CARTESIAN_POINT ( 'NONE',  ( 8.000000000000000000, 13.55483219355744673, -11.06713717293225407 ) ) ;
#25757=ORIENTED_EDGE ( 'NONE', *, *, #12507, .T. ) ;
#25760=EDGE_CURVE ( 'NONE', #26513, #17877, #27506, .T. ) ;
#25790=CIRCLE ( 'NONE', #2213, 17.49900000000002720 ) ;
#25795=VERTEX_POINT ( 'NONE', #34133 ) ;
#25806=CARTESIAN_POINT ( 'NONE',  ( 0.000000000000000000, -6.336799421339930127, 16.31134495048480915 ) ) ;
#25812=ADVANCED_FACE ( 'NONE', ( #22958 ), #22778, .T. ) ;
#25815=CARTESIAN_POINT ( 'NONE',  ( 8.000000000000000000, 0.000000000000000000, 0.000000000000000000 ) ) ;
#25816=DIRECTION ( 'NONE',  ( -1.000000000000000000, 0.000000000000000000, 0.000000000000000000 ) ) ;
#25817=EDGE_CURVE ( 'NONE', #21217, #3103, #8417, .T. ) ;
#25818=ORIENTED_EDGE ( 'NONE', *, *, #30318, .F. ) ;
#25833=ORIENTED_EDGE ( 'NONE', *, *, #9015, .T. ) ;
#25838=VERTEX_POINT ( 'NONE', #17015 ) ;
#25841=ORIENTED_EDGE ( 'NONE', *, *, #2464, .T. ) ;
#25851=AXIS2_PLACEMENT_3D ( 'NONE', #280, #17001, #25666 ) ;
#25857=CARTESIAN_POINT ( 'NONE',  ( 8.000000000000000000, 18.48663108841359559, -3.384281271887881637 ) ) ;
#25873=FACE_OUTER_BOUND ( 'NONE', #31895, .T. ) ;
#25890=ADVANCED_FACE ( 'NONE', ( #27845 ), #14668, .T. ) ;
#25897=FACE_OUTER_BOUND ( 'NONE', #32963, .T. ) ;
#25908=ORIENTED_EDGE ( 'NONE', *, *, #11207, .F. ) ;
#25919=ORIENTED_EDGE ( 'NONE', *, *, #30598, .T. ) ;
#25925=ORIENTED_EDGE ( 'NONE', *, *, #5536, .T. ) ;
#25933=VECTOR ( 'NONE', #13525, 1000.000000000000000 ) ;
#25948=ORIENTED_EDGE ( 'NONE', *, *, #14161, .T. ) ;
#25952=ORIENTED_EDGE ( 'NONE', *, *, #31040, .T. ) ;
#25959=EDGE_CURVE ( 'NONE', #27460, #13434, #31250, .T. ) ;
#25961=CARTESIAN_POINT ( 'NONE',  ( 4.000000000000003553, -19.35373470438990395, 10.46102064772334295 ) ) ;
#25968=ORIENTED_EDGE ( 'NONE', *, *, #34379, .T. ) ;
#25974=ORIENTED_EDGE ( 'NONE', *, *, #27407, .F. ) ;
#25978=CARTESIAN_POINT ( 'NONE',  ( 8.000000000000000000, 0.000000000000000000, 0.000000000000000000 ) ) ;
#25981=VECTOR ( 'NONE', #13829, 1000.000000000000000 ) ;
#25983=ADVANCED_FACE ( 'NONE', ( #31779 ), #28735, .T. ) ;
#26002=CARTESIAN_POINT ( 'NONE',  ( 0.000000000000000000, 15.92965478239619515, 15.17386234660388844 ) ) ;
#26003=ORIENTED_EDGE ( 'NONE', *, *, #27880, .F. ) ;
#26004=ORIENTED_EDGE ( 'NONE', *, *, #22729, .F. ) ;
#26014=ADVANCED_FACE ( 'NONE', ( #12524 ), #23502, .T. ) ;
#26024=CARTESIAN_POINT ( 'NONE',  ( 0.000000000000000000, -18.48663108841361336, 3.384281271887747078 ) ) ;
#26033=CARTESIAN_POINT ( 'NONE',  ( 0.000000000000000000, 6.336799421339804894, 16.31134495048487310 ) ) ;
#26045=CARTESIAN_POINT ( 'NONE',  ( 8.000000000000000000, 13.55483219355729396, 11.06713717293245658 ) ) ;
#26051=FACE_OUTER_BOUND ( 'NONE', #15642, .T. ) ;
#26069=AXIS2_PLACEMENT_3D ( 'NONE', #2435, #7993, #24745 ) ;
#26079=CIRCLE ( 'NONE', #23761, 8.000000000000007105 ) ;
#26109=CARTESIAN_POINT ( 'NONE',  ( 8.000000000000000000, 0.000000000000000000, 0.000000000000000000 ) ) ;
#26115=CYLINDRICAL_SURFACE ( 'NONE', #28571, 17.49900000000000233 ) ;
#26117=DIRECTION ( 'NONE',  ( 0.000000000000000000, 0.000000000000000000, 1.000000000000000000 ) ) ;
#26121=ORIENTED_EDGE ( 'NONE', *, *, #31500, .T. ) ;
#26128=CIRCLE ( 'NONE', #23237, 8.000000000000008882 ) ;
#26150=AXIS2_PLACEMENT_3D ( 'NONE', #9854, #29136, #4489 ) ;
#26172=AXIS2_PLACEMENT_3D ( 'NONE', #15551, #32137, #6935 ) ;
#26182=VERTEX_POINT ( 'NONE', #13249 ) ;
#26188=AXIS2_PLACEMENT_3D ( 'NONE', #28459, #30800, #6664 ) ;
#26194=EDGE_CURVE ( 'NONE', #251, #4339, #35573, .T. ) ;
#26218=VERTEX_POINT ( 'NONE', #32856 ) ;
#26229=AXIS2_PLACEMENT_3D ( 'NONE', #34366, #6622, #22638 ) ;
#26236=ORIENTED_EDGE ( 'NONE', *, *, #18719, .F. ) ;
#26244=CYLINDRICAL_SURFACE ( 'NONE', #27256, 4.000000000000000000 ) ;
#26264=AXIS2_PLACEMENT_3D ( 'NONE', #1690, #28872, #15163 ) ;
#26268=AXIS2_PLACEMENT_3D ( 'NONE', #27319, #2317, #24266 ) ;
#26285=AXIS2_PLACEMENT_3D ( 'NONE', #18452, #12888, #29449 ) ;
#26290=AXIS2_PLACEMENT_3D ( 'NONE', #15552, #1908, #10177 ) ;
#26308=ORIENTED_EDGE ( 'NONE', *, *, #31500, .F. ) ;
#26309=DIRECTION ( 'NONE',  ( -1.000000000000000000, 0.000000000000000000, 0.000000000000000000 ) ) ;
#26313=DIRECTION ( 'NONE',  ( 1.000000000000000000, -0.000000000000000000, -0.000000000000000000 ) ) ;
#26327=ORIENTED_EDGE ( 'NONE', *, *, #5103, .F. ) ;
#26345=CARTESIAN_POINT ( 'NONE',  ( -10.00000000000000178, 0.000000000000000000, 0.000000000000000000 ) ) ;
#26366=( NAMED_UNIT ( * ) PLANE_ANGLE_UNIT ( ) SI_UNIT ( $, .RADIAN. ) );
#26375=CARTESIAN_POINT ( 'NONE',  ( 4.000000000000003553, 19.83898331853685448, 9.508666619816713350 ) ) ;
#26397=DIRECTION ( 'NONE',  ( 0.000000000000000000, 0.000000000000000000, 1.000000000000000000 ) ) ;
#26400=ORIENTED_EDGE ( 'NONE', *, *, #22741, .T. ) ;
#26412=AXIS2_PLACEMENT_3D ( 'NONE', #11609, #33236, #14132 ) ;
#26424=DIRECTION ( 'NONE',  ( -1.000000000000000000, 0.000000000000000000, 0.000000000000000000 ) ) ;
#26426=FACE_OUTER_BOUND ( 'NONE', #5292, .T. ) ;
#26444=ORIENTED_EDGE ( 'NONE', *, *, #23066, .T. ) ;
#26448=FACE_OUTER_BOUND ( 'NONE', #18021, .T. ) ;
#26451=STYLED_ITEM ( 'NONE', ( #24972 ), #10370 ) ;
#26452=CARTESIAN_POINT ( 'NONE',  ( 0.000000000000000000, 9.508666619816942500, -19.83898331853677632 ) ) ;
#26468=ORIENTED_EDGE ( 'NONE', *, *, #23949, .F. ) ;
#26499=EDGE_LOOP ( 'NONE', ( #28847, #17606, #9514, #7704 ) ) ;
#26502=CIRCLE ( 'NONE', #27064, 17.49900000000000233 ) ;
#26513=VERTEX_POINT ( 'NONE', #29547 ) ;
#26517=CARTESIAN_POINT ( 'NONE',  ( 8.000000000000000000, 4.460989585141205360, -16.92083251265323085 ) ) ;
#26532=CARTESIAN_POINT ( 'NONE',  ( 0.000000000000000000, 0.000000000000000000, 0.000000000000000000 ) ) ;
#26563=DIRECTION ( 'NONE',  ( -1.000000000000000000, 0.000000000000000000, 0.000000000000000000 ) ) ;
#26569=DIRECTION ( 'NONE',  ( -1.000000000000000000, 0.000000000000000000, 0.000000000000000000 ) ) ;
#26575=CARTESIAN_POINT ( 'NONE',  ( 8.000000000000000000, 2.494040418455619523, -18.62763138773847871 ) ) ;
#26583=VERTEX_POINT ( 'NONE', #5063 ) ;
#26589=CARTESIAN_POINT ( 'NONE',  ( 0.000000000000000000, 0.000000000000000000, 0.000000000000000000 ) ) ;
#26591=ORIENTED_EDGE ( 'NONE', *, *, #12357, .T. ) ;
#26597=VERTEX_POINT ( 'NONE', #32059 ) ;
#26606=DIRECTION ( 'NONE',  ( -1.000000000000000000, 0.000000000000000000, 0.000000000000000000 ) ) ;
#26612=DIRECTION ( 'NONE',  ( 0.000000000000000000, -0.9510565162951502005, -0.3090169943749580539 ) ) ;
#26621=AXIS2_PLACEMENT_3D ( 'NONE', #18841, #32709, #4996 ) ;
#26627=AXIS2_PLACEMENT_3D ( 'NONE', #21489, #32482, #7815 ) ;
#26629=DIRECTION ( 'NONE',  ( -1.000000000000000000, 0.000000000000000000, 0.000000000000000000 ) ) ;
#26641=CARTESIAN_POINT ( 'NONE',  ( 0.000000000000000000, -17.47118961583598917, -0.9861715913089493801 ) ) ;
#26656=DIRECTION ( 'NONE',  ( 0.000000000000000000, -0.5877852522924621459, -0.8090169943749555559 ) ) ;
#26672=VERTEX_POINT ( 'NONE', #25203 ) ;
#26683=CIRCLE ( 'NONE', #17444, 8.000000000000015987 ) ;
#26688=EDGE_CURVE ( 'NONE', #5984, #26597, #30174, .T. ) ;
#26695=EDGE_LOOP ( 'NONE', ( #25818, #15843, #7892, #3031 ) ) ;
#26705=AXIS2_PLACEMENT_3D ( 'NONE', #6285, #19759, #28256 ) ;
#26709=DIRECTION ( 'NONE',  ( -1.000000000000000000, 0.000000000000000000, 0.000000000000000000 ) ) ;
#26715=DIRECTION ( 'NONE',  ( -1.000000000000000000, 0.000000000000000000, 0.000000000000000000 ) ) ;
#26729=EDGE_LOOP ( 'NONE', ( #31884, #8442, #27761, #23545, #11468, #27733, #1701, #25414, #24503, #8184, #24887, #9926, #9952, #12999, #23696, #18061, #29409, #5558, #2633, #14865, #15313, #23115, #14258, #9829, #18289, #20335, #34860, #11894, #8234, #8596, #356, #2378, #24292, #4551, #24352, #27114, #32200, #11827, #29332, #5022, #37, #14511, #18558, #27174, #24938, #20299, #19001, #11393, #12312, #25948, #13781, #15140, #2297, #34589, #25692, #33054, #11571, #27130, #20419, #23460, #11118, #17738, #4696, #16623, #20734, #11757, #18282, #33797, #760, #1025, #26772, #28672, #6505, #33443, #32458, #15609, #31043, #31493, #10, #10302, #30089, #25968, #13693, #9923, #3835 ) ) ;
#26742=DIRECTION ( 'NONE',  ( 1.000000000000000000, -0.000000000000000000, 0.000000000000000000 ) ) ;
#26772=ORIENTED_EDGE ( 'NONE', *, *, #16990, .F. ) ;
#26778=DIRECTION ( 'NONE',  ( -1.000000000000000000, 0.000000000000000000, 0.000000000000000000 ) ) ;
#26781=DIRECTION ( 'NONE',  ( -1.000000000000000000, 0.000000000000000000, 0.000000000000000000 ) ) ;
#26792=DIRECTION ( 'NONE',  ( 0.000000000000000000, -1.000000000000000000, -1.040834085586082363E-14 ) ) ;
#26818=ORIENTED_EDGE ( 'NONE', *, *, #31954, .F. ) ;
#26832=DIRECTION ( 'NONE',  ( 0.000000000000000000, 0.000000000000000000, 1.000000000000000000 ) ) ;
#26833=AXIS2_PLACEMENT_3D ( 'NONE', #11185, #3274, #554 ) ;
#26844=EDGE_CURVE ( 'NONE', #15127, #21342, #2013, .T. ) ;
#26854=AXIS2_PLACEMENT_3D ( 'NONE', #22114, #2881, #13845 ) ;
#26858=VERTEX_POINT ( 'NONE', #25736 ) ;
#26866=ORIENTED_EDGE ( 'NONE', *, *, #30407, .F. ) ;
#26911=DIRECTION ( 'NONE',  ( 0.000000000000000000, 0.3090169943749412895, 0.9510565162951555296 ) ) ;
#26912=ORIENTED_EDGE ( 'NONE', *, *, #25082, .F. ) ;
#26920=DIRECTION ( 'NONE',  ( 0.000000000000000000, 0.000000000000000000, 1.000000000000000000 ) ) ;
#26925=EDGE_CURVE ( 'NONE', #27973, #4339, #19250, .T. ) ;
#26943=CARTESIAN_POINT ( 'NONE',  ( 8.000000000000000000, -15.17386234660370015, -15.92965478239635679 ) ) ;
#26949=DIRECTION ( 'NONE',  ( -1.000000000000000000, 0.000000000000000000, 0.000000000000000000 ) ) ;
#26950=DIRECTION ( 'NONE',  ( 0.000000000000000000, 0.000000000000000000, 1.000000000000000000 ) ) ;
#26958=CARTESIAN_POINT ( 'NONE',  ( 0.000000000000000000, -16.31134495048486954, 6.336799421339753380 ) ) ;
#26975=DIRECTION ( 'NONE',  ( 0.000000000000000000, 0.3090169943749477288, -0.9510565162951535312 ) ) ;
#26997=ORIENTED_EDGE ( 'NONE', *, *, #34625, .T. ) ;
#27018=EDGE_LOOP ( 'NONE', ( #7309, #2834, #3277, #24078 ) ) ;
#27034=CARTESIAN_POINT ( 'NONE',  ( 8.000000000000000000, -17.47118961583602470, 0.9861715913087032437 ) ) ;
#27040=LINE ( 'NONE', #2214, #25933 ) ;
#27045=ADVANCED_FACE ( 'NONE', ( #35261 ), #32012, .T. ) ;
#27052=DIRECTION ( 'NONE',  ( 1.000000000000000000, -0.000000000000000000, -0.000000000000000000 ) ) ;
#27064=AXIS2_PLACEMENT_3D ( 'NONE', #18664, #15959, #4486 ) ;
#27071=VERTEX_POINT ( 'NONE', #29498 ) ;
#27076=EDGE_LOOP ( 'NONE', ( #6344, #27767, #29164, #34227 ) ) ;
#27079=SURFACE_SIDE_STYLE ('',( #30127 ) ) ;
#27080=LINE ( 'NONE', #30128, #23879 ) ;
#27081=VERTEX_POINT ( 'NONE', #13297 ) ;
#27085=AXIS2_PLACEMENT_3D ( 'NONE', #33714, #19493, #27627 ) ;
#27089=CARTESIAN_POINT ( 'NONE',  ( 8.000000000000000000, -9.471478019455027209, -14.71414642875966017 ) ) ;
#27099=ORIENTED_EDGE ( 'NONE', *, *, #18052, .T. ) ;
#27103=CARTESIAN_POINT ( 'NONE',  ( 8.000000000000000000, 12.96676809804150565, 13.60411018104323411 ) ) ;
#27114=ORIENTED_EDGE ( 'NONE', *, *, #7507, .T. ) ;
#27116=CARTESIAN_POINT ( 'NONE',  ( 8.000000000000000000, 0.000000000000000000, 0.000000000000000000 ) ) ;
#27120=ORIENTED_EDGE ( 'NONE', *, *, #29066, .T. ) ;
#27130=ORIENTED_EDGE ( 'NONE', *, *, #1659, .T. ) ;
#27132=EDGE_CURVE ( 'NONE', #31502, #31127, #24626, .T. ) ;
#27134=ORIENTED_EDGE ( 'NONE', *, *, #5536, .F. ) ;
#27138=CARTESIAN_POINT ( 'NONE',  ( 8.000000000000000000, -9.508666619816786181, 19.83898331853681896 ) ) ;
#27169=AXIS2_PLACEMENT_3D ( 'NONE', #29837, #21178, #12910 ) ;
#27170=AXIS2_PLACEMENT_3D ( 'NONE', #28534, #33572, #28716 ) ;
#27174=ORIENTED_EDGE ( 'NONE', *, *, #4006, .T. ) ;
#27180=CARTESIAN_POINT ( 'NONE',  ( 8.000000000000000000, -18.62763138773852134, 2.494040418455287345 ) ) ;
#27209=AXIS2_PLACEMENT_3D ( 'NONE', #24007, #13201, #18585 ) ;
#27210=AXIS2_PLACEMENT_3D ( 'NONE', #1352, #28723, #28896 ) ;
#27214=VERTEX_POINT ( 'NONE', #14151 ) ;
#27249=EDGE_LOOP ( 'NONE', ( #25428, #2249, #19821, #10275 ) ) ;
#27256=AXIS2_PLACEMENT_3D ( 'NONE', #23717, #4825, #4294 ) ;
#27280=ORIENTED_EDGE ( 'NONE', *, *, #8152, .T. ) ;
#27293=DIRECTION ( 'NONE',  ( -1.000000000000000000, 0.000000000000000000, 0.000000000000000000 ) ) ;
#27319=CARTESIAN_POINT ( 'NONE',  ( 0.000000000000000000, 18.48663108841359559, -3.384281271887881637 ) ) ;
#27335=EDGE_LOOP ( 'NONE', ( #6331, #23465, #15032, #25237 ) ) ;
#27344=CARTESIAN_POINT ( 'NONE',  ( 8.000000000000000000, 18.48663108841356717, 3.384281271888136988 ) ) ;
#27359=ADVANCED_FACE ( 'NONE', ( #25873 ), #33787, .T. ) ;
#27394=ADVANCED_FACE ( 'NONE', ( #12713 ), #34321, .T. ) ;
#27398=ORIENTED_EDGE ( 'NONE', *, *, #34385, .T. ) ;
#27400=CIRCLE ( 'NONE', #26833, 8.000000000000007105 ) ;
#27407=EDGE_CURVE ( 'NONE', #15604, #12176, #24459, .T. ) ;
#27411=VECTOR ( 'NONE', #23137, 1000.000000000000000 ) ;
#27418=AXIS2_PLACEMENT_3D ( 'NONE', #18532, #12786, #23951 ) ;
#27437=( NAMED_UNIT ( * ) PLANE_ANGLE_UNIT ( ) SI_UNIT ( $, .RADIAN. ) );
#27439=CARTESIAN_POINT ( 'NONE',  ( 8.000000000000000000, 12.96676809804168862, -13.60411018104304048 ) ) ;
#27440=VERTEX_POINT ( 'NONE', #1917 ) ;
#27443=DIRECTION ( 'NONE',  ( 0.000000000000000000, 0.000000000000000000, 1.000000000000000000 ) ) ;
#27454=DIRECTION ( 'NONE',  ( 0.000000000000000000, 0.000000000000000000, 1.000000000000000000 ) ) ;
#27456=DIRECTION ( 'NONE',  ( -1.000000000000000000, 0.000000000000000000, 0.000000000000000000 ) ) ;
#27460=VERTEX_POINT ( 'NONE', #26943 ) ;
#27462=DIRECTION ( 'NONE',  ( 1.000000000000000000, -0.000000000000000000, -0.000000000000000000 ) ) ;
#27496=DIRECTION ( 'NONE',  ( 0.000000000000000000, -0.8090169943749534465, 0.5877852522924650325 ) ) ;
#27506=LINE ( 'NONE', #2845, #23349 ) ;
#27509=FACE_OUTER_BOUND ( 'NONE', #30630, .T. ) ;
#27512=VECTOR ( 'NONE', #7357, 1000.000000000000000 ) ;
#27543=FACE_OUTER_BOUND ( 'NONE', #35107, .T. ) ;
#27567=EDGE_CURVE ( 'NONE', #251, #17877, #15263, .T. ) ;
#27582=ADVANCED_FACE ( 'NONE', ( #35579 ), #2818, .T. ) ;
#27597=DIRECTION ( 'NONE',  ( -1.000000000000000000, 0.000000000000000000, 0.000000000000000000 ) ) ;
#27598=CARTESIAN_POINT ( 'NONE',  ( -10.00000000000000178, 0.000000000000000000, 0.000000000000000000 ) ) ;
#27627=DIRECTION ( 'NONE',  ( 1.000000000000000000, -0.000000000000000000, 0.000000000000000000 ) ) ;
#27647=DIRECTION ( 'NONE',  ( -1.000000000000000000, 0.000000000000000000, 0.000000000000000000 ) ) ;
#27669=DIRECTION ( 'NONE',  ( 0.000000000000000000, 0.000000000000000000, 1.000000000000000000 ) ) ;
#27684=CIRCLE ( 'NONE', #2967, 8.000000000000001776 ) ;
#27686=CARTESIAN_POINT ( 'NONE',  ( 8.000000000000000000, 11.06713717293261467, -13.55483219355716606 ) ) ;
#27694=ADVANCED_FACE ( 'NONE', ( #8009 ), #5499, .T. ) ;
#27698=AXIS2_PLACEMENT_3D ( 'NONE', #21521, #13448, #29655 ) ;
#27705=CIRCLE ( 'NONE', #1856, 8.000000000000005329 ) ;
#27718=DIRECTION ( 'NONE',  ( 0.000000000000000000, 0.000000000000000000, -1.000000000000000000 ) ) ;
#27729=EDGE_LOOP ( 'NONE', ( #797, #15838, #32849, #12167 ) ) ;
#27733=ORIENTED_EDGE ( 'NONE', *, *, #30436, .T. ) ;
#27734=CIRCLE ( 'NONE', #9906, 22.00000000000000000 ) ;
#27736=FACE_OUTER_BOUND ( 'NONE', #16885, .T. ) ;
#27744=CIRCLE ( 'NONE', #30613, 8.000000000000014211 ) ;
#27754=VECTOR ( 'NONE', #24378, 1000.000000000000000 ) ;
#27761=ORIENTED_EDGE ( 'NONE', *, *, #23845, .F. ) ;
#27763=ORIENTED_EDGE ( 'NONE', *, *, #1409, .T. ) ;
#27767=ORIENTED_EDGE ( 'NONE', *, *, #11957, .T. ) ;
#27770=ORIENTED_EDGE ( 'NONE', *, *, #24081, .T. ) ;
#27784=ORIENTED_EDGE ( 'NONE', *, *, #66, .F. ) ;
#27807=ADVANCED_FACE ( 'NONE', ( #22389, #22922 ), #8706, .F. ) ;
#27828=ORIENTED_EDGE ( 'NONE', *, *, #3793, .F. ) ;
#27832=CARTESIAN_POINT ( 'NONE',  ( 0.000000000000000000, -2.912696353505970226, 21.80633394113446499 ) ) ;
#27834=DIRECTION ( 'NONE',  ( -1.000000000000000000, 0.000000000000000000, -0.000000000000000000 ) ) ;
#27845=FACE_OUTER_BOUND ( 'NONE', #33839, .T. ) ;
#27849=DIRECTION ( 'NONE',  ( -1.000000000000000000, 0.000000000000000000, 0.000000000000000000 ) ) ;
#27852=DIRECTION ( 'NONE',  ( -1.000000000000000000, 0.000000000000000000, 0.000000000000000000 ) ) ;
#27862=CYLINDRICAL_SURFACE ( 'NONE', #5073, 17.49900000000000233 ) ;
#27865=VERTEX_POINT ( 'NONE', #6722 ) ;
#27871=DIRECTION ( 'NONE',  ( -1.000000000000000000, 0.000000000000000000, 0.000000000000000000 ) ) ;
#27876=CYLINDRICAL_SURFACE ( 'NONE', #23632, 22.00000000000000000 ) ;
#27880=EDGE_CURVE ( 'NONE', #4678, #34729, #3335, .T. ) ;
#27894=VERTEX_POINT ( 'NONE', #28701 ) ;
#27902=CYLINDRICAL_SURFACE ( 'NONE', #10951, 17.49900000000000233 ) ;
#27913=EDGE_CURVE ( 'NONE', #24278, #1617, #4049, .T. ) ;
#27914=VERTEX_POINT ( 'NONE', #34814 ) ;
#27920=EDGE_CURVE ( 'NONE', #24278, #9536, #34276, .T. ) ;
#27922=CARTESIAN_POINT ( 'NONE',  ( 8.000000000000000000, -18.62763138773852134, 10.49404041845529001 ) ) ;
#27950=CARTESIAN_POINT ( 'NONE',  ( 8.000000000000000000, 0.000000000000000000, 17.49900000000000233 ) ) ;
#27951=ORIENTED_EDGE ( 'NONE', *, *, #19723, .T. ) ;
#27973=VERTEX_POINT ( 'NONE', #24838 ) ;
#27978=CIRCLE ( 'NONE', #12452, 8.000000000000007105 ) ;
#27980=CIRCLE ( 'NONE', #13613, 8.000000000000001776 ) ;
#28031=VECTOR ( 'NONE', #32173, 1000.000000000000000 ) ;
#28046=AXIS2_PLACEMENT_3D ( 'NONE', #35226, #21502, #92 ) ;
#28052=DIRECTION ( 'NONE',  ( 0.000000000000000000, -0.3090169943749350723, -0.9510565162951576390 ) ) ;
#28058=CIRCLE ( 'NONE', #12530, 17.49900000000000233 ) ;
#28072=DIRECTION ( 'NONE',  ( -1.000000000000000000, 0.000000000000000000, 0.000000000000000000 ) ) ;
#28142=PRODUCT_DEFINITION_CONTEXT ( 'detailed design', #24379, 'design' ) ;
#28146=CYLINDRICAL_SURFACE ( 'NONE', #32243, 8.000000000000000000 ) ;
#28150=CARTESIAN_POINT ( 'NONE',  ( 8.000000000000000000, -12.96676809804157848, 13.60411018104313641 ) ) ;
#28162=EDGE_CURVE ( 'NONE', #27460, #7117, #10114, .T. ) ;
#28181=CIRCLE ( 'NONE', #2323, 8.000000000000008882 ) ;
#28183=FACE_OUTER_BOUND ( 'NONE', #24607, .T. ) ;
#28186=FACE_OUTER_BOUND ( 'NONE', #29900, .T. ) ;
#28228=EDGE_LOOP ( 'NONE', ( #9332, #21778, #4895, #8786 ) ) ;
#28256=DIRECTION ( 'NONE',  ( 0.000000000000000000, -0.3090169943749546677, 0.9510565162951511997 ) ) ;
#28261=ORIENTED_EDGE ( 'NONE', *, *, #8034, .T. ) ;
#28271=CARTESIAN_POINT ( 'NONE',  ( 8.000000000000000000, -18.48663108841356717, -3.384281271888017084 ) ) ;
#28275=EDGE_CURVE ( 'NONE', #29296, #11194, #34881, .T. ) ;
#28307=CARTESIAN_POINT ( 'NONE',  ( 0.000000000000000000, 18.62763138773855687, 10.49404041845541968 ) ) ;
#28326=EDGE_CURVE ( 'NONE', #34692, #6495, #3264, .T. ) ;
#28328=DIRECTION ( 'NONE',  ( -1.000000000000000000, 0.000000000000000000, 0.000000000000000000 ) ) ;
#28333=AXIS2_PLACEMENT_3D ( 'NONE', #31857, #7190, #18169 ) ;
#28339=DIRECTION ( 'NONE',  ( 0.000000000000000000, 0.5877852522924739143, -0.8090169943749468962 ) ) ;
#28357=DIRECTION ( 'NONE',  ( 0.000000000000000000, -0.9510565162951502005, -0.3090169943749580539 ) ) ;
#28388=EDGE_CURVE ( 'NONE', #16289, #272, #21043, .T. ) ;
#28405=DIRECTION ( 'NONE',  ( -1.000000000000000000, 0.000000000000000000, 0.000000000000000000 ) ) ;
#28426=ORIENTED_EDGE ( 'NONE', *, *, #6134, .F. ) ;
#28428=CARTESIAN_POINT ( 'NONE',  ( 8.000000000000000000, 0.000000000000000000, 0.000000000000000000 ) ) ;
#28432=AXIS2_PLACEMENT_3D ( 'NONE', #24809, #132, #11123 ) ;
#28455=EDGE_CURVE ( 'NONE', #27081, #4678, #31985, .T. ) ;
#28459=CARTESIAN_POINT ( 'NONE',  ( 0.000000000000000000, 18.62763138773856397, -2.494040418455147456 ) ) ;
#28483=ORIENTED_EDGE ( 'NONE', *, *, #16140, .F. ) ;
#28488=CIRCLE ( 'NONE', #35387, 17.49900000000001299 ) ;
#28504=DIRECTION ( 'NONE',  ( 1.000000000000000000, -0.000000000000000000, 0.000000000000000000 ) ) ;
#28524=EDGE_LOOP ( 'NONE', ( #32210, #3484, #17123, #26400 ) ) ;
#28534=CARTESIAN_POINT ( 'NONE',  ( 8.000000000000000000, 0.000000000000000000, 0.000000000000000000 ) ) ;
#28538=CYLINDRICAL_SURFACE ( 'NONE', #3968, 8.000000000000001776 ) ;
#28539=VECTOR ( 'NONE', #16749, 1000.000000000000000 ) ;
#28554=CARTESIAN_POINT ( 'NONE',  ( 4.000000000000003553, -15.17386234660370370, -15.92965478239635679 ) ) ;
#28571=AXIS2_PLACEMENT_3D ( 'NONE', #25586, #9894, #6661 ) ;
#28575=DIRECTION ( 'NONE',  ( -1.000000000000000000, 0.000000000000000000, 0.000000000000000000 ) ) ;
#28579=CARTESIAN_POINT ( 'NONE',  ( -10.00000000000000178, 0.000000000000000000, 0.000000000000000000 ) ) ;
#28597=VECTOR ( 'NONE', #8349, 1000.000000000000000 ) ;
#28611=EDGE_CURVE ( 'NONE', #22897, #15158, #27978, .T. ) ;
#28614=ORIENTED_EDGE ( 'NONE', *, *, #25274, .F. ) ;
#28672=ORIENTED_EDGE ( 'NONE', *, *, #19792, .T. ) ;
#28691=CYLINDRICAL_SURFACE ( 'NONE', #6199, 17.49900000000000233 ) ;
#28701=CARTESIAN_POINT ( 'NONE',  ( 8.000000000000000000, 21.63912866391140000, 3.968388925834891001 ) ) ;
#28704=VECTOR ( 'NONE', #30835, 1000.000000000000000 ) ;
#28709=ORIENTED_EDGE ( 'NONE', *, *, #31047, .T. ) ;
#28716=DIRECTION ( 'NONE',  ( 0.000000000000000000, 0.000000000000000000, 1.000000000000000000 ) ) ;
#28718=LINE ( 'NONE', #26375, #16104 ) ;
#28721=EDGE_CURVE ( 'NONE', #31502, #23346, #33728, .T. ) ;
#28723=DIRECTION ( 'NONE',  ( -1.000000000000000000, 0.000000000000000000, 0.000000000000000000 ) ) ;
#28735=CYLINDRICAL_SURFACE ( 'NONE', #21081, 8.000000000000000000 ) ;
#28753=AXIS2_PLACEMENT_3D ( 'NONE', #28760, #23897, #1218 ) ;
#28760=CARTESIAN_POINT ( 'NONE',  ( 8.000000000000000000, -16.53603053422202862, -8.931325931664767737 ) ) ;
#28768=DIRECTION ( 'NONE',  ( 0.000000000000000000, 0.000000000000000000, 1.000000000000000000 ) ) ;
#28798=VERTEX_POINT ( 'NONE', #643 ) ;
#28803=AXIS2_PLACEMENT_3D ( 'NONE', #7132, #6778, #20619 ) ;
#28809=DIRECTION ( 'NONE',  ( -1.000000000000000000, 0.000000000000000000, 0.000000000000000000 ) ) ;
#28816=DIRECTION ( 'NONE',  ( -1.000000000000000000, 0.000000000000000000, 0.000000000000000000 ) ) ;
#28818=ORIENTED_EDGE ( 'NONE', *, *, #14298, .F. ) ;
#28845=AXIS2_PLACEMENT_3D ( 'NONE', #32520, #10928, #16297 ) ;
#28847=ORIENTED_EDGE ( 'NONE', *, *, #31496, .F. ) ;
#28872=DIRECTION ( 'NONE',  ( -1.000000000000000000, 0.000000000000000000, 0.000000000000000000 ) ) ;
#28873=ORIENTED_EDGE ( 'NONE', *, *, #11732, .F. ) ;
#28892=DIRECTION ( 'NONE',  ( -1.000000000000000000, 0.000000000000000000, 0.000000000000000000 ) ) ;
#28896=DIRECTION ( 'NONE',  ( 0.000000000000000000, 0.000000000000000000, 1.000000000000000000 ) ) ;
#28900=VECTOR ( 'NONE', #29286, 1000.000000000000000 ) ;
#28909=DIRECTION ( 'NONE',  ( 0.000000000000000000, 0.000000000000000000, 1.000000000000000000 ) ) ;
#28914=DIRECTION ( 'NONE',  ( 0.000000000000000000, 0.000000000000000000, 1.000000000000000000 ) ) ;
#28917=AXIS2_PLACEMENT_3D ( 'NONE', #26532, #4751, #6711 ) ;
#28928=ADVANCED_FACE ( 'NONE', ( #7642 ), #7473, .T. ) ;
#28930=AXIS2_PLACEMENT_3D ( 'NONE', #22330, #19964, #25044 ) ;
#28935=EDGE_LOOP ( 'NONE', ( #3915, #35383, #17263, #24420 ) ) ;
#28936=DIRECTION ( 'NONE',  ( 0.000000000000000000, 0.9510565162951523099, 0.3090169943749513926 ) ) ;
#28938=ORIENTED_EDGE ( 'NONE', *, *, #18719, .T. ) ;
#28939=DIRECTION ( 'NONE',  ( 0.000000000000000000, 0.000000000000000000, 1.000000000000000000 ) ) ;
#28941=FACE_OUTER_BOUND ( 'NONE', #1820, .T. ) ;
#28962=ORIENTED_EDGE ( 'NONE', *, *, #12766, .F. ) ;
#28964=CARTESIAN_POINT ( 'NONE',  ( 0.000000000000000000, 8.128228055638880178, 16.94522934049213347 ) ) ;
#29008=LINE ( 'NONE', #25961, #24552 ) ;
#29017=VERTEX_POINT ( 'NONE', #16452 ) ;
#29018=VERTEX_POINT ( 'NONE', #32858 ) ;
#29030=CARTESIAN_POINT ( 'NONE',  ( 0.000000000000000000, -10.46102064772325413, -19.35373470438994659 ) ) ;
#29036=VERTEX_POINT ( 'NONE', #8178 ) ;
#29063=ORIENTED_EDGE ( 'NONE', *, *, #30371, .T. ) ;
#29066=EDGE_CURVE ( 'NONE', #29835, #30763, #18990, .T. ) ;
#29076=CIRCLE ( 'NONE', #35411, 22.00000000000000000 ) ;
#29077=CARTESIAN_POINT ( 'NONE',  ( 0.000000000000000000, 12.96676809804168862, -13.60411018104304048 ) ) ;
#29083=AXIS2_PLACEMENT_3D ( 'NONE', #31020, #3140, #33540 ) ;
#29096=DIRECTION ( 'NONE',  ( -1.000000000000000000, 0.000000000000000000, 0.000000000000000000 ) ) ;
#29097=DIRECTION ( 'NONE',  ( 0.000000000000000000, -0.8090169943749534465, 0.5877852522924650325 ) ) ;
#29107=ORIENTED_EDGE ( 'NONE', *, *, #19792, .F. ) ;
#29134=CIRCLE ( 'NONE', #14742, 22.00000000000000000 ) ;
#29136=DIRECTION ( 'NONE',  ( -1.000000000000000000, 0.000000000000000000, 0.000000000000000000 ) ) ;
#29150=CARTESIAN_POINT ( 'NONE',  ( 50.00005079999999680, 3.872983346207416133, -1.000000000000000000 ) ) ;
#29157=ORIENTED_EDGE ( 'NONE', *, *, #35066, .T. ) ;
#29164=ORIENTED_EDGE ( 'NONE', *, *, #14635, .T. ) ;
#29170=VERTEX_POINT ( 'NONE', #25641 ) ;
#29178=CIRCLE ( 'NONE', #15294, 22.00000000000000000 ) ;
#29182=DIRECTION ( 'NONE',  ( -1.000000000000000000, 0.000000000000000000, 0.000000000000000000 ) ) ;
#29251=CARTESIAN_POINT ( 'NONE',  ( 8.000000000000000000, -6.336799421339700977, -16.31134495048491573 ) ) ;
#29255=CYLINDRICAL_SURFACE ( 'NONE', #30978, 22.00000000000000000 ) ;
#29256=CARTESIAN_POINT ( 'NONE',  ( 0.000000000000000000, 0.000000000000000000, 0.000000000000000000 ) ) ;
#29269=CARTESIAN_POINT ( 'NONE',  ( 4.000000000000003553, -19.83898331853694685, 9.508666619816580123 ) ) ;
#29278=ADVANCED_FACE ( 'NONE', ( #19672 ), #14453, .T. ) ;
#29286=DIRECTION ( 'NONE',  ( -0.000000000000000000, 1.000000000000000000, 0.000000000000000000 ) ) ;
#29289=ORIENTED_EDGE ( 'NONE', *, *, #312, .F. ) ;
#29296=VERTEX_POINT ( 'NONE', #27034 ) ;
#29298=DIRECTION ( 'NONE',  ( -1.000000000000000000, 0.000000000000000000, 0.000000000000000000 ) ) ;
#29302=DIRECTION ( 'NONE',  ( 0.000000000000000000, 0.000000000000000000, 1.000000000000000000 ) ) ;
#29318=CARTESIAN_POINT ( 'NONE',  ( 8.000000000000000000, -13.60411018104326963, 12.96676809804144348 ) ) ;
#29327=VERTEX_POINT ( 'NONE', #18728 ) ;
#29332=ORIENTED_EDGE ( 'NONE', *, *, #34360, .T. ) ;
#29343=EDGE_CURVE ( 'NONE', #21628, #4187, #12504, .T. ) ;
#29382=DIRECTION ( 'NONE',  ( 0.000000000000000000, 0.5877852522924739143, -0.8090169943749468962 ) ) ;
#29403=CYLINDRICAL_SURFACE ( 'NONE', #3173, 22.00000000000000000 ) ;
#29406=DIRECTION ( 'NONE',  ( 0.000000000000000000, 0.000000000000000000, 1.000000000000000000 ) ) ;
#29409=ORIENTED_EDGE ( 'NONE', *, *, #8909, .T. ) ;
#29424=ORIENTED_EDGE ( 'NONE', *, *, #13421, .T. ) ;
#29427=CIRCLE ( 'NONE', #23687, 8.000000000000010658 ) ;
#29430=DIRECTION ( 'NONE',  ( 0.000000000000000000, 0.9510565162951545304, -0.3090169943749448977 ) ) ;
#29439=DIRECTION ( 'NONE',  ( -1.000000000000000000, 0.000000000000000000, 0.000000000000000000 ) ) ;
#29449=DIRECTION ( 'NONE',  ( 0.000000000000000000, 0.000000000000000000, 1.000000000000000000 ) ) ;
#29460=DIRECTION ( 'NONE',  ( 1.000000000000000000, -0.000000000000000000, -0.000000000000000000 ) ) ;
#29463=ORIENTED_EDGE ( 'NONE', *, *, #6169, .F. ) ;
#29481=ORIENTED_EDGE ( 'NONE', *, *, #21144, .T. ) ;
#29484=DIRECTION ( 'NONE',  ( -1.000000000000000000, 0.000000000000000000, 0.000000000000000000 ) ) ;
#29490=CARTESIAN_POINT ( 'NONE',  ( 8.000000000000000000, -18.48663108841361336, 3.384281271887747078 ) ) ;
#29498=CARTESIAN_POINT ( 'NONE',  ( 0.000000000000000000, 15.17386234660384581, 15.92965478239621824 ) ) ;
#29508=VECTOR ( 'NONE', #8712, 1000.000000000000000 ) ;
#29547=CARTESIAN_POINT ( 'NONE',  ( 0.000000000000000000, -9.508666619816789733, 19.83898331853681896 ) ) ;
#29552=EDGE_CURVE ( 'NONE', #27214, #11860, #6766, .T. ) ;
#29608=AXIS2_PLACEMENT_3D ( 'NONE', #18317, #7861, #26792 ) ;
#29621=LINE ( 'NONE', #24925, #21119 ) ;
#29631=DIRECTION ( 'NONE',  ( -1.000000000000000000, 0.000000000000000000, 0.000000000000000000 ) ) ;
#29650=ORIENTED_EDGE ( 'NONE', *, *, #22256, .F. ) ;
#29655=DIRECTION ( 'NONE',  ( 0.000000000000000000, 0.000000000000000000, 1.000000000000000000 ) ) ;
#29679=AXIS2_PLACEMENT_3D ( 'NONE', #28150, #25089, #14273 ) ;
#29724=DIRECTION ( 'NONE',  ( 0.000000000000000000, 0.000000000000000000, 1.000000000000000000 ) ) ;
#29756=CIRCLE ( 'NONE', #1017, 17.49900000000001299 ) ;
#29760=EDGE_CURVE ( 'NONE', #4678, #6546, #22874, .T. ) ;
#29766=CIRCLE ( 'NONE', #25726, 8.000000000000007105 ) ;
#29771=AXIS2_PLACEMENT_3D ( 'NONE', #7833, #26949, #21334 ) ;
#29783=DIRECTION ( 'NONE',  ( -1.000000000000000000, 0.000000000000000000, 0.000000000000000000 ) ) ;
#29814=CARTESIAN_POINT ( 'NONE',  ( 50.00005079999999680, 0.000000000000000000, 4.000000000000000000 ) ) ;
#29815=AXIS2_PLACEMENT_3D ( 'NONE', #21037, #4157, #20320 ) ;
#29816=AXIS2_PLACEMENT_3D ( 'NONE', #24610, #25310, #3177 ) ;
#29819=ORIENTED_EDGE ( 'NONE', *, *, #4605, .T. ) ;
#29831=DIRECTION ( 'NONE',  ( 0.000000000000000000, 0.000000000000000000, 1.000000000000000000 ) ) ;
#29835=VERTEX_POINT ( 'NONE', #29866 ) ;
#29837=CARTESIAN_POINT ( 'NONE',  ( 8.000000000000000000, 0.000000000000000000, 0.000000000000000000 ) ) ;
#29842=CYLINDRICAL_SURFACE ( 'NONE', #5067, 22.00000000000000000 ) ;
#29852=SURFACE_SIDE_STYLE ('',( #35427 ) ) ;
#29862=ORIENTED_EDGE ( 'NONE', *, *, #14845, .F. ) ;
#29864=ORIENTED_EDGE ( 'NONE', *, *, #26194, .T. ) ;
#29866=CARTESIAN_POINT ( 'NONE',  ( 0.000000000000000000, 2.912696353506125657, -21.80633394113447210 ) ) ;
#29891=DIRECTION ( 'NONE',  ( 0.000000000000000000, 0.3090169943749415116, 0.9510565162951555296 ) ) ;
#29900=EDGE_LOOP ( 'NONE', ( #5425, #19125, #31297, #13874 ) ) ;
#29919=CARTESIAN_POINT ( 'NONE',  ( 8.000000000000000000, 18.62763138773856397, -2.494040418455147456 ) ) ;
#29940=ORIENTED_EDGE ( 'NONE', *, *, #17437, .F. ) ;
#29948=ORIENTED_EDGE ( 'NONE', *, *, #22069, .T. ) ;
#29951=ORIENTED_EDGE ( 'NONE', *, *, #21374, .T. ) ;
#29994=DIRECTION ( 'NONE',  ( 0.000000000000000000, -0.5877852522924797984, 0.8090169943749425663 ) ) ;
#30052=VERTEX_POINT ( 'NONE', #26452 ) ;
#30087=DIRECTION ( 'NONE',  ( -1.000000000000000000, 0.000000000000000000, 0.000000000000000000 ) ) ;
#30089=ORIENTED_EDGE ( 'NONE', *, *, #954, .T. ) ;
#30097=LINE ( 'NONE', #5091, #30975 ) ;
#30107=DIRECTION ( 'NONE',  ( -1.000000000000000000, 0.000000000000000000, 0.000000000000000000 ) ) ;
#30112=EDGE_CURVE ( 'NONE', #2115, #24515, #32118, .T. ) ;
#30118=VECTOR ( 'NONE', #23454, 1000.000000000000000 ) ;
#30127=SURFACE_STYLE_FILL_AREA ( #21650 ) ;
#30128=CARTESIAN_POINT ( 'NONE',  ( 50.00005079999999680, 3.872983346207429900, 1.000000000000003109 ) ) ;
#30163=ORIENTED_EDGE ( 'NONE', *, *, #34394, .F. ) ;
#30174=CIRCLE ( 'NONE', #13005, 8.000000000000008882 ) ;
#30184=DIRECTION ( 'NONE',  ( -1.000000000000000000, 0.000000000000000000, 0.000000000000000000 ) ) ;
#30189=CARTESIAN_POINT ( 'NONE',  ( 0.000000000000000000, 14.71414642875970635, -9.471478019454975694 ) ) ;
#30217=EDGE_CURVE ( 'NONE', #9536, #27440, #32496, .T. ) ;
#30220=ORIENTED_EDGE ( 'NONE', *, *, #19171, .F. ) ;
#30227=VECTOR ( 'NONE', #31521, 1000.000000000000000 ) ;
#30274=CIRCLE ( 'NONE', #26264, 8.000000000000007105 ) ;
#30290=DIRECTION ( 'NONE',  ( 0.000000000000000000, 0.000000000000000000, 1.000000000000000000 ) ) ;
#30312=VERTEX_POINT ( 'NONE', #7614 ) ;
#30318=EDGE_CURVE ( 'NONE', #4713, #19206, #15232, .T. ) ;
#30321=FACE_OUTER_BOUND ( 'NONE', #4556, .T. ) ;
#30343=CARTESIAN_POINT ( 'NONE',  ( 8.000000000000000000, 5.400000000000013678, 5.082197683525802034E-18 ) ) ;
#30359=FACE_OUTER_BOUND ( 'NONE', #2004, .T. ) ;
#30361=CARTESIAN_POINT ( 'NONE',  ( 4.000000000000003553, 9.508666619816651178, 19.83898331853691488 ) ) ;
#30366=DIRECTION ( 'NONE',  ( -1.000000000000000000, 0.000000000000000000, 0.000000000000000000 ) ) ;
#30370=CARTESIAN_POINT ( 'NONE',  ( 0.000000000000000000, -10.46102064772354723, 19.35373470438981869 ) ) ;
#30371=EDGE_CURVE ( 'NONE', #9304, #30389, #27080, .T. ) ;
#30383=ORIENTED_EDGE ( 'NONE', *, *, #4006, .F. ) ;
#30386=CARTESIAN_POINT ( 'NONE',  ( 0.000000000000000000, 0.000000000000000000, 0.000000000000000000 ) ) ;
#30389=VERTEX_POINT ( 'NONE', #24731 ) ;
#30407=EDGE_CURVE ( 'NONE', #25593, #22962, #12951, .T. ) ;
#30417=CYLINDRICAL_SURFACE ( 'NONE', #26854, 17.49900000000000233 ) ;
#30422=CARTESIAN_POINT ( 'NONE',  ( 0.000000000000000000, -13.60411018104308667, -12.96676809804163000 ) ) ;
#30436=EDGE_CURVE ( 'NONE', #26597, #18803, #25601, .T. ) ;
#30461=VECTOR ( 'NONE', #23574, 1000.000000000000000 ) ;
#30466=ORIENTED_EDGE ( 'NONE', *, *, #31972, .T. ) ;
#30470=DIRECTION ( 'NONE',  ( -1.000000000000000000, 0.000000000000000000, 0.000000000000000000 ) ) ;
#30475=VECTOR ( 'NONE', #19868, 1000.000000000000000 ) ;
#30478=VERTEX_POINT ( 'NONE', #25072 ) ;
#30484=VERTEX_POINT ( 'NONE', #28307 ) ;
#30491=EDGE_LOOP ( 'NONE', ( #29107, #10873, #29951, #15514 ) ) ;
#30500=CARTESIAN_POINT ( 'NONE',  ( 8.000000000000000000, -16.94522934049206597, -8.128228055639052485 ) ) ;
#30501=CIRCLE ( 'NONE', #13817, 22.00000000000000000 ) ;
#30511=CARTESIAN_POINT ( 'NONE',  ( 8.000000000000000000, 2.494040418455352182, 18.62763138773848937 ) ) ;
#30519=FACE_OUTER_BOUND ( 'NONE', #5031, .T. ) ;
#30547=( GEOMETRIC_REPRESENTATION_CONTEXT ( 3 ) GLOBAL_UNCERTAINTY_ASSIGNED_CONTEXT ( ( #17860 ) ) GLOBAL_UNIT_ASSIGNED_CONTEXT ( ( #34474, #26366, #34650 ) ) REPRESENTATION_CONTEXT ( 'NONE', 'WORKASPACE' ) );
#30553=ORIENTED_EDGE ( 'NONE', *, *, #16886, .F. ) ;
#30564=EDGE_CURVE ( 'NONE', #25573, #25593, #11824, .T. ) ;
#30598=EDGE_CURVE ( 'NONE', #34183, #16691, #25615, .T. ) ;
#30603=CARTESIAN_POINT ( 'NONE',  ( 0.000000000000000000, 0.000000000000000000, 0.000000000000000000 ) ) ;
#30613=AXIS2_PLACEMENT_3D ( 'NONE', #3499, #11754, #20020 ) ;
#30621=AXIS2_PLACEMENT_3D ( 'NONE', #18788, #2073, #26920 ) ;
#30630=EDGE_LOOP ( 'NONE', ( #18332, #25974, #18627, #4441 ) ) ;
#30633=CARTESIAN_POINT ( 'NONE',  ( 0.000000000000000000, -4.460989585141084568, 16.92083251265323440 ) ) ;
#30695=DIRECTION ( 'NONE',  ( -1.000000000000000000, 0.000000000000000000, 0.000000000000000000 ) ) ;
#30707=CARTESIAN_POINT ( 'NONE',  ( 0.000000000000000000, 0.000000000000000000, 0.000000000000000000 ) ) ;
#30712=DIRECTION ( 'NONE',  ( -1.000000000000000000, 0.000000000000000000, 0.000000000000000000 ) ) ;
#30730=VERTEX_POINT ( 'NONE', #12640 ) ;
#30732=DIRECTION ( 'NONE',  ( -1.000000000000000000, 0.000000000000000000, 0.000000000000000000 ) ) ;
#30741=VECTOR ( 'NONE', #30732, 1000.000000000000000 ) ;
#30746=CARTESIAN_POINT ( 'NONE',  ( 8.000000000000000000, 0.000000000000000000, 0.000000000000000000 ) ) ;
#30756=CARTESIAN_POINT ( 'NONE',  ( 0.000000000000000000, 0.000000000000000000, 0.000000000000000000 ) ) ;
#30763=VERTEX_POINT ( 'NONE', #9752 ) ;
#30796=CIRCLE ( 'NONE', #15262, 8.000000000000007105 ) ;
#30797=AXIS2_PLACEMENT_3D ( 'NONE', #15385, #18278, #1729 ) ;
#30799=DIRECTION ( 'NONE',  ( 0.000000000000000000, 0.000000000000000000, -1.000000000000000000 ) ) ;
#30800=DIRECTION ( 'NONE',  ( 1.000000000000000000, -0.000000000000000000, 0.000000000000000000 ) ) ;
#30802=ORIENTED_EDGE ( 'NONE', *, *, #11474, .T. ) ;
#30814=VERTEX_POINT ( 'NONE', #18562 ) ;
#30818=AXIS2_PLACEMENT_3D ( 'NONE', #15338, #18762, #20742 ) ;
#30835=DIRECTION ( 'NONE',  ( -1.000000000000000000, 0.000000000000000000, 0.000000000000000000 ) ) ;
#30839=EDGE_CURVE ( 'NONE', #4881, #24556, #27040, .T. ) ;
#30852=EDGE_CURVE ( 'NONE', #26218, #9081, #6358, .T. ) ;
#30853=ORIENTED_EDGE ( 'NONE', *, *, #22729, .T. ) ;
#30859=AXIS2_PLACEMENT_3D ( 'NONE', #34494, #7108, #15374 ) ;
#30862=DIRECTION ( 'NONE',  ( 0.000000000000000000, 0.000000000000000000, -1.000000000000000000 ) ) ;
#30865=CARTESIAN_POINT ( 'NONE',  ( 0.000000000000000000, -11.06713717293229138, -13.55483219355740765 ) ) ;
#30886=ADVANCED_FACE ( 'NONE', ( #13707 ), #32079, .T. ) ;
#30898=DIRECTION ( 'NONE',  ( 1.000000000000000000, -0.000000000000000000, -0.000000000000000000 ) ) ;
#30914=ADVANCED_FACE ( 'NONE', ( #21787 ), #5258, .T. ) ;
#30930=LINE ( 'NONE', #26517, #8716 ) ;
#30941=CARTESIAN_POINT ( 'NONE',  ( 8.000000000000000000, -16.53603053422215297, 8.931325931664547468 ) ) ;
#30950=VERTEX_POINT ( 'NONE', #16195 ) ;
#30955=ADVANCED_FACE ( 'NONE', ( #34975 ), #18382, .T. ) ;
#30957=ORIENTED_EDGE ( 'NONE', *, *, #14731, .F. ) ;
#30975=VECTOR ( 'NONE', #27052, 1000.000000000000000 ) ;
#30978=AXIS2_PLACEMENT_3D ( 'NONE', #15179, #7451, #18428 ) ;
#30984=LINE ( 'NONE', #19793, #32171 ) ;
#31001=AXIS2_PLACEMENT_3D ( 'NONE', #31459, #12911, #31807 ) ;
#31009=AXIS2_PLACEMENT_3D ( 'NONE', #29318, #1770, #18319 ) ;
#31020=CARTESIAN_POINT ( 'NONE',  ( 8.000000000000000000, -2.494040418455211849, -18.62763138773853200 ) ) ;
#31021=DIRECTION ( 'NONE',  ( 0.000000000000000000, 0.000000000000000000, 1.000000000000000000 ) ) ;
#31033=MECHANICAL_DESIGN_GEOMETRIC_PRESENTATION_REPRESENTATION('',(#26451),#20087);
#31040=EDGE_CURVE ( 'NONE', #16592, #12885, #32962, .T. ) ;
#31043=ORIENTED_EDGE ( 'NONE', *, *, #26925, .T. ) ;
#31047=EDGE_CURVE ( 'NONE', #11860, #23663, #24857, .T. ) ;
#31055=EDGE_CURVE ( 'NONE', #29036, #6031, #31094, .T. ) ;
#31073=CARTESIAN_POINT ( 'NONE',  ( -10.00000000000000178, 0.000000000000000000, 0.000000000000000000 ) ) ;
#31074=DIRECTION ( 'NONE',  ( -1.000000000000000000, 0.000000000000000000, 0.000000000000000000 ) ) ;
#31080=EDGE_CURVE ( 'NONE', #29170, #18178, #22142, .T. ) ;
#31094=CIRCLE ( 'NONE', #46, 8.000000000000001776 ) ;
#31096=DIRECTION ( 'NONE',  ( 0.000000000000000000, 0.000000000000000000, 1.000000000000000000 ) ) ;
#31102=DIRECTION ( 'NONE',  ( -1.000000000000000000, 0.000000000000000000, 0.000000000000000000 ) ) ;
#31120=ADVANCED_FACE ( 'NONE', ( #12049 ), #1429, .T. ) ;
#31127=VERTEX_POINT ( 'NONE', #15445 ) ;
#31177=ORIENTED_EDGE ( 'NONE', *, *, #31405, .T. ) ;
#31185=VECTOR ( 'NONE', #10841, 1000.000000000000000 ) ;
#31188=ORIENTED_EDGE ( 'NONE', *, *, #34379, .F. ) ;
#31224=CIRCLE ( 'NONE', #15685, 8.000000000000007105 ) ;
#31250=LINE ( 'NONE', #28554, #27411 ) ;
#31263=VECTOR ( 'NONE', #29439, 1000.000000000000000 ) ;
#31275=AXIS2_PLACEMENT_3D ( 'NONE', #22551, #16795, #33024 ) ;
#31281=CARTESIAN_POINT ( 'NONE',  ( 8.000000000000000000, -9.471478019455243924, 14.71414642875952161 ) ) ;
#31295=FACE_OUTER_BOUND ( 'NONE', #34417, .T. ) ;
#31297=ORIENTED_EDGE ( 'NONE', *, *, #7988, .T. ) ;
#31320=EDGE_CURVE ( 'NONE', #12885, #180, #27684, .T. ) ;
#31336=AXIS2_PLACEMENT_3D ( 'NONE', #34850, #17730, #15373 ) ;
#31363=LINE ( 'NONE', #3837, #21212 ) ;
#31376=AXIS2_PLACEMENT_3D ( 'NONE', #34041, #6311, #23226 ) ;
#31390=VECTOR ( 'NONE', #10325, 1000.000000000000000 ) ;
#31393=CARTESIAN_POINT ( 'NONE',  ( 8.000000000000000000, 18.62763138773855687, 2.494040418455418351 ) ) ;
#31405=EDGE_CURVE ( 'NONE', #1847, #1074, #5215, .T. ) ;
#31408=VECTOR ( 'NONE', #33337, 1000.000000000000000 ) ;
#31424=CIRCLE ( 'NONE', #15889, 22.00000000000000000 ) ;
#31433=VERTEX_POINT ( 'NONE', #26641 ) ;
#31442=ORIENTED_EDGE ( 'NONE', *, *, #16521, .T. ) ;
#31459=CARTESIAN_POINT ( 'NONE',  ( 0.000000000000000000, 0.000000000000000000, 0.000000000000000000 ) ) ;
#31477=CARTESIAN_POINT ( 'NONE',  ( 8.000000000000000000, -17.47118961583598917, -0.9861715913089493801 ) ) ;
#31489=CARTESIAN_POINT ( 'NONE',  ( 8.000000000000000000, 0.000000000000000000, 0.000000000000000000 ) ) ;
#31493=ORIENTED_EDGE ( 'NONE', *, *, #66, .T. ) ;
#31496=EDGE_CURVE ( 'NONE', #2828, #30730, #16689, .T. ) ;
#31500=EDGE_CURVE ( 'NONE', #30478, #25573, #5857, .T. ) ;
#31502=VERTEX_POINT ( 'NONE', #22979 ) ;
#31503=ORIENTED_EDGE ( 'NONE', *, *, #11946, .F. ) ;
#31506=CARTESIAN_POINT ( 'NONE',  ( 8.000000000000000000, -10.46102064772325413, -19.35373470438994303 ) ) ;
#31520=ORIENTED_EDGE ( 'NONE', *, *, #34780, .F. ) ;
#31521=DIRECTION ( 'NONE',  ( -1.000000000000000000, 0.000000000000000000, 0.000000000000000000 ) ) ;
#31601=CARTESIAN_POINT ( 'NONE',  ( -10.00000000000000178, 0.000000000000000000, 0.000000000000000000 ) ) ;
#31603=CARTESIAN_POINT ( 'NONE',  ( 0.000000000000000000, 0.000000000000000000, 0.000000000000000000 ) ) ;
#31621=VECTOR ( 'NONE', #9288, 1000.000000000000000 ) ;
#31639=CIRCLE ( 'NONE', #17264, 22.00000000000000000 ) ;
#31649=VECTOR ( 'NONE', #25436, 1000.000000000000000 ) ;
#31657=ADVANCED_FACE ( 'NONE', ( #22801 ), #33802, .T. ) ;
#31665=ORIENTED_EDGE ( 'NONE', *, *, #282, .T. ) ;
#31676=FACE_OUTER_BOUND ( 'NONE', #15937, .T. ) ;
#31693=VERTEX_POINT ( 'NONE', #3736 ) ;
#31767=CARTESIAN_POINT ( 'NONE',  ( 8.000000000000000000, 15.17386234660384581, 15.92965478239621824 ) ) ;
#31779=FACE_OUTER_BOUND ( 'NONE', #23919, .T. ) ;
#31799=AXIS2_PLACEMENT_3D ( 'NONE', #27103, #10359, #16627 ) ;
#31800=CIRCLE ( 'NONE', #28333, 17.49900000000001654 ) ;
#31807=DIRECTION ( 'NONE',  ( 0.000000000000000000, -0.9510565162951565288, 0.3090169943749384029 ) ) ;
#31823=CARTESIAN_POINT ( 'NONE',  ( 8.000000000000000000, -16.94522934049218676, 8.128228055638807348 ) ) ;
#31827=DIRECTION ( 'NONE',  ( 0.000000000000000000, 0.8090169943749448977, 0.5877852522924766898 ) ) ;
#31832=DIRECTION ( 'NONE',  ( 0.000000000000000000, 0.3090169943749477288, -0.9510565162951535312 ) ) ;
#31838=AXIS2_PLACEMENT_3D ( 'NONE', #13577, #7629, #27454 ) ;
#31848=CIRCLE ( 'NONE', #15152, 8.000000000000008882 ) ;
#31855=CARTESIAN_POINT ( 'NONE',  ( 8.000000000000000000, 0.000000000000000000, 0.000000000000000000 ) ) ;
#31857=CARTESIAN_POINT ( 'NONE',  ( 8.000000000000000000, 0.000000000000000000, 0.000000000000000000 ) ) ;
#31879=ORIENTED_EDGE ( 'NONE', *, *, #24914, .T. ) ;
#31884=ORIENTED_EDGE ( 'NONE', *, *, #24604, .T. ) ;
#31895=EDGE_LOOP ( 'NONE', ( #13344, #1163, #4939, #9218 ) ) ;
#31918=CARTESIAN_POINT ( 'NONE',  ( 0.000000000000000000, 0.9861715913090087771, -17.47118961583601049 ) ) ;
#31932=EDGE_LOOP ( 'NONE', ( #22839, #11206, #23926, #11631 ) ) ;
#31944=ADVANCED_FACE ( 'NONE', ( #16825 ), #10918, .T. ) ;
#31948=AXIS2_PLACEMENT_3D ( 'NONE', #11239, #2624, #13941 ) ;
#31949=DIRECTION ( 'NONE',  ( 0.000000000000000000, 0.3090169943749415116, 0.9510565162951555296 ) ) ;
#31954=EDGE_CURVE ( 'NONE', #6627, #29835, #27734, .T. ) ;
#31956=DIRECTION ( 'NONE',  ( 0.000000000000000000, 0.000000000000000000, 1.000000000000000000 ) ) ;
#31972=EDGE_CURVE ( 'NONE', #32783, #26597, #24955, .T. ) ;
#31982=DIRECTION ( 'NONE',  ( -1.000000000000000000, 0.000000000000000000, 0.000000000000000000 ) ) ;
#31985=CIRCLE ( 'NONE', #7254, 8.000000000000007105 ) ;
#31994=CIRCLE ( 'NONE', #22775, 8.000000000000005329 ) ;
#31999=FACE_OUTER_BOUND ( 'NONE', #18823, .T. ) ;
#32008=DIRECTION ( 'NONE',  ( 0.000000000000000000, -0.9510565162951500895, -0.3090169943749579429 ) ) ;
#32012=CYLINDRICAL_SURFACE ( 'NONE', #22687, 8.000000000000001776 ) ;
#32033=ORIENTED_EDGE ( 'NONE', *, *, #27567, .F. ) ;
#32049=CARTESIAN_POINT ( 'NONE',  ( 8.000000000000000000, -12.96676809804139197, -13.60411018104332292 ) ) ;
#32052=ORIENTED_EDGE ( 'NONE', *, *, #19318, .F. ) ;
#32059=CARTESIAN_POINT ( 'NONE',  ( 0.000000000000000000, 9.508666619816651178, 19.83898331853691488 ) ) ;
#32079=PLANE ( 'NONE',  #22464 ) ;
#32099=CARTESIAN_POINT ( 'NONE',  ( 0.000000000000000000, -0.9861715913088822116, 17.47118961583599273 ) ) ;
#32103=EDGE_CURVE ( 'NONE', #31127, #11512, #11616, .T. ) ;
#32118=LINE ( 'NONE', #29251, #16394 ) ;
#32126=LINE ( 'NONE', #4949, #34530 ) ;
#32137=DIRECTION ( 'NONE',  ( -1.000000000000000000, 0.000000000000000000, 0.000000000000000000 ) ) ;
#32139=ORIENTED_EDGE ( 'NONE', *, *, #21565, .T. ) ;
#32142=DIRECTION ( 'NONE',  ( 0.000000000000000000, -0.5877852522924621459, -0.8090169943749553338 ) ) ;
#32151=VERTEX_POINT ( 'NONE', #22579 ) ;
#32153=DIRECTION ( 'NONE',  ( -1.000000000000000000, 0.000000000000000000, 0.000000000000000000 ) ) ;
#32157=ADVANCED_FACE ( 'NONE', ( #28183 ), #23295, .T. ) ;
#32163=DIRECTION ( 'NONE',  ( 0.000000000000000000, 0.000000000000000000, 1.000000000000000000 ) ) ;
#32169=CARTESIAN_POINT ( 'NONE',  ( 8.000000000000000000, 16.31134495048494060, -6.336799421339643246 ) ) ;
#32171=VECTOR ( 'NONE', #33334, 1000.000000000000000 ) ;
#32173=DIRECTION ( 'NONE',  ( 1.000000000000000000, -0.000000000000000000, -0.000000000000000000 ) ) ;
#32200=ORIENTED_EDGE ( 'NONE', *, *, #20900, .F. ) ;
#32210=ORIENTED_EDGE ( 'NONE', *, *, #19957, .F. ) ;
#32213=CARTESIAN_POINT ( 'NONE',  ( 8.000000000000000000, 3.872983346207416133, -1.000000000000000000 ) ) ;
#32219=DIRECTION ( 'NONE',  ( 1.000000000000000000, -0.000000000000000000, -0.000000000000000000 ) ) ;
#32228=CARTESIAN_POINT ( 'NONE',  ( 8.000000000000000000, 0.000000000000000000, 0.000000000000000000 ) ) ;
#32232=LINE ( 'NONE', #8085, #4858 ) ;
#32236=ADVANCED_FACE ( 'NONE', ( #9090 ), #996, .T. ) ;
#32243=AXIS2_PLACEMENT_3D ( 'NONE', #13925, #3488, #14438 ) ;
#32294=EDGE_LOOP ( 'NONE', ( #13641, #21563, #21882, #8855 ) ) ;
#32300=DIRECTION ( 'NONE',  ( -1.000000000000000000, 0.000000000000000000, 0.000000000000000000 ) ) ;
#32331=ORIENTED_EDGE ( 'NONE', *, *, #2077, .F. ) ;
#32350=DIRECTION ( 'NONE',  ( 0.000000000000000000, 0.000000000000000000, -1.000000000000000000 ) ) ;
#32355=CARTESIAN_POINT ( 'NONE',  ( 0.000000000000000000, -0.9861715913086358531, -17.47118961583604957 ) ) ;
#32366=DIRECTION ( 'NONE',  ( -1.000000000000000000, 0.000000000000000000, 0.000000000000000000 ) ) ;
#32388=CIRCLE ( 'NONE', #5939, 17.49900000000002720 ) ;
#32398=FACE_OUTER_BOUND ( 'NONE', #28935, .T. ) ;
#32404=EDGE_CURVE ( 'NONE', #9009, #3103, #2475, .T. ) ;
#32411=ORIENTED_EDGE ( 'NONE', *, *, #4421, .F. ) ;
#32426=EDGE_CURVE ( 'NONE', #30950, #5984, #15647, .T. ) ;
#32429=DIRECTION ( 'NONE',  ( 0.000000000000000000, 0.3090169943749477288, -0.9510565162951534202 ) ) ;
#32433=EDGE_CURVE ( 'NONE', #32783, #19338, #13946, .T. ) ;
#32436=EDGE_CURVE ( 'NONE', #519, #21217, #35555, .T. ) ;
#32458=ORIENTED_EDGE ( 'NONE', *, *, #21395, .F. ) ;
#32477=CARTESIAN_POINT ( 'NONE',  ( 8.000000000000000000, -11.06713717293248855, 13.55483219355725844 ) ) ;
#32482=DIRECTION ( 'NONE',  ( -1.000000000000000000, 0.000000000000000000, 0.000000000000000000 ) ) ;
#32496=CIRCLE ( 'NONE', #11222, 8.000000000000000000 ) ;
#32503=ORIENTED_EDGE ( 'NONE', *, *, #20929, .T. ) ;
#32507=ORIENTED_EDGE ( 'NONE', *, *, #13421, .F. ) ;
#32508=CYLINDRICAL_SURFACE ( 'NONE', #35035, 8.000000000000001776 ) ;
#32509=ADVANCED_FACE ( 'NONE', ( #8157 ), #16243, .T. ) ;
#32513=AXIS2_PLACEMENT_3D ( 'NONE', #4437, #23682, #32142 ) ;
#32520=CARTESIAN_POINT ( 'NONE',  ( 0.000000000000000000, -18.48663108841356717, -3.384281271888017084 ) ) ;
#32526=VECTOR ( 'NONE', #3414, 1000.000000000000000 ) ;
#32533=CARTESIAN_POINT ( 'NONE',  ( 4.000000000000003553, -3.968388925834960723, 21.63912866391138934 ) ) ;
#32570=DIRECTION ( 'NONE',  ( -1.000000000000000000, 0.000000000000000000, 0.000000000000000000 ) ) ;
#32589=CARTESIAN_POINT ( 'NONE',  ( 50.00005079999999680, 5.400000000000021672, 1.000000000000001776 ) ) ;
#32600=ORIENTED_EDGE ( 'NONE', *, *, #13092, .F. ) ;
#32605=DIRECTION ( 'NONE',  ( -1.000000000000000000, 0.000000000000000000, 0.000000000000000000 ) ) ;
#32613=ORIENTED_EDGE ( 'NONE', *, *, #33275, .T. ) ;
#32625=EDGE_CURVE ( 'NONE', #32655, #34510, #34030, .T. ) ;
#32630=DIRECTION ( 'NONE',  ( -1.000000000000000000, 0.000000000000000000, 0.000000000000000000 ) ) ;
#32643=LINE ( 'NONE', #23829, #3859 ) ;
#32650=( LENGTH_UNIT ( ) NAMED_UNIT ( * ) SI_UNIT ( .MILLI., .METRE. ) );
#32655=VERTEX_POINT ( 'NONE', #9535 ) ;
#32657=DIRECTION ( 'NONE',  ( -1.000000000000000000, 0.000000000000000000, 0.000000000000000000 ) ) ;
#32666=DIRECTION ( 'NONE',  ( 0.000000000000000000, 0.8090169943749448977, 0.5877852522924766898 ) ) ;
#32667=CARTESIAN_POINT ( 'NONE',  ( 0.000000000000000000, 0.000000000000000000, 0.000000000000000000 ) ) ;
#32687=CARTESIAN_POINT ( 'NONE',  ( 8.000000000000000000, 0.000000000000000000, 0.000000000000000000 ) ) ;
#32692=CARTESIAN_POINT ( 'NONE',  ( 0.000000000000000000, -2.912696353505664248, -21.80633394113455736 ) ) ;
#32700=ORIENTED_EDGE ( 'NONE', *, *, #10815, .F. ) ;
#32705=CARTESIAN_POINT ( 'NONE',  ( 8.000000000000000000, 0.000000000000000000, 0.000000000000000000 ) ) ;
#32709=DIRECTION ( 'NONE',  ( -1.000000000000000000, 0.000000000000000000, 0.000000000000000000 ) ) ;
#32738=VERTEX_POINT ( 'NONE', #23754 ) ;
#32742=ORIENTED_EDGE ( 'NONE', *, *, #32768, .T. ) ;
#32764=PRODUCT_DEFINITION_FORMATION_WITH_SPECIFIED_SOURCE ( 'ANY', '', #34550, .NOT_KNOWN. ) ;
#32767=ORIENTED_EDGE ( 'NONE', *, *, #18491, .F. ) ;
#32768=EDGE_CURVE ( 'NONE', #29296, #35453, #1622, .T. ) ;
#32769=ORIENTED_EDGE ( 'NONE', *, *, #12221, .T. ) ;
#32779=CIRCLE ( 'NONE', #22994, 17.49900000000000944 ) ;
#32782=DIRECTION ( 'NONE',  ( 0.000000000000000000, 0.000000000000000000, 1.000000000000000000 ) ) ;
#32783=VERTEX_POINT ( 'NONE', #34743 ) ;
#32785=CIRCLE ( 'NONE', #9777, 22.00000000000000000 ) ;
#32797=CARTESIAN_POINT ( 'NONE',  ( 8.000000000000000000, -16.31134495048487310, 6.336799421339755156 ) ) ;
#32800=FACE_OUTER_BOUND ( 'NONE', #12583, .T. ) ;
#32809=ADVANCED_FACE ( 'NONE', ( #18345 ), #18877, .T. ) ;
#32830=ORIENTED_EDGE ( 'NONE', *, *, #22224, .F. ) ;
#32849=ORIENTED_EDGE ( 'NONE', *, *, #30852, .F. ) ;
#32856=CARTESIAN_POINT ( 'NONE',  ( 0.000000000000000000, 16.92083251265324861, 4.460989585141029501 ) ) ;
#32858=CARTESIAN_POINT ( 'NONE',  ( 0.000000000000000000, 0.9861715913087641949, 17.47118961583601759 ) ) ;
#32871=AXIS2_PLACEMENT_3D ( 'NONE', #20100, #28405, #3748 ) ;
#32886=DIRECTION ( 'NONE',  ( -1.000000000000000000, 0.000000000000000000, 0.000000000000000000 ) ) ;
#32916=CIRCLE ( 'NONE', #21978, 17.49900000000000233 ) ;
#32924=ORIENTED_EDGE ( 'NONE', *, *, #31320, .F. ) ;
#32926=AXIS2_PLACEMENT_3D ( 'NONE', #19109, #30107, #5446 ) ;
#32962=LINE ( 'NONE', #538, #33397 ) ;
#32963=EDGE_LOOP ( 'NONE', ( #12908, #11635, #1863, #32600 ) ) ;
#32985=DIRECTION ( 'NONE',  ( 0.000000000000000000, 0.9510565162951523099, 0.3090169943749513926 ) ) ;
#32997=LINE ( 'NONE', #8311, #22214 ) ;
#33005=CIRCLE ( 'NONE', #22644, 22.00000000000000000 ) ;
#33018=PLANE ( 'NONE',  #27085 ) ;
#33024=DIRECTION ( 'NONE',  ( 0.000000000000000000, 0.000000000000000000, 1.000000000000000000 ) ) ;
#33032=ORIENTED_EDGE ( 'NONE', *, *, #32625, .F. ) ;
#33053=ORIENTED_EDGE ( 'NONE', *, *, #25760, .F. ) ;
#33054=ORIENTED_EDGE ( 'NONE', *, *, #6183, .T. ) ;
#33072=CARTESIAN_POINT ( 'NONE',  ( 8.000000000000000000, 19.35373470438985422, 10.46102064772347795 ) ) ;
#33086=CARTESIAN_POINT ( 'NONE',  ( 0.000000000000000000, -15.92965478239607968, -15.17386234660401101 ) ) ;
#33089=ADVANCED_FACE ( 'NONE', ( #16866 ), #22105, .T. ) ;
#33113=DIRECTION ( 'NONE',  ( -1.000000000000000000, 0.000000000000000000, 0.000000000000000000 ) ) ;
#33202=ADVANCED_FACE ( 'NONE', ( #15931 ), #13429, .T. ) ;
#33204=ORIENTED_EDGE ( 'NONE', *, *, #3176, .F. ) ;
#33233=EDGE_CURVE ( 'NONE', #22962, #23663, #7905, .T. ) ;
#33236=DIRECTION ( 'NONE',  ( -1.000000000000000000, 0.000000000000000000, 0.000000000000000000 ) ) ;
#33253=ORIENTED_EDGE ( 'NONE', *, *, #25097, .T. ) ;
#33263=CARTESIAN_POINT ( 'NONE',  ( 4.000000000000003553, 19.35373470438985777, 10.46102064772347795 ) ) ;
#33275=EDGE_CURVE ( 'NONE', #25710, #2681, #18832, .T. ) ;
#33276=DIRECTION ( 'NONE',  ( 0.000000000000000000, -0.5877852522924621459, -0.8090169943749553338 ) ) ;
#33288=CARTESIAN_POINT ( 'NONE',  ( 8.000000000000000000, -16.94522934049218676, 8.128228055638807348 ) ) ;
#33308=ORIENTED_EDGE ( 'NONE', *, *, #28326, .T. ) ;
#33317=EDGE_CURVE ( 'NONE', #15169, #31693, #10799, .T. ) ;
#33334=DIRECTION ( 'NONE',  ( -1.000000000000000000, 0.000000000000000000, 0.000000000000000000 ) ) ;
#33337=DIRECTION ( 'NONE',  ( -1.000000000000000000, 0.000000000000000000, 0.000000000000000000 ) ) ;
#33342=CIRCLE ( 'NONE', #17799, 17.49900000000001654 ) ;
#33353=DIRECTION ( 'NONE',  ( 0.000000000000000000, 0.000000000000000000, 1.000000000000000000 ) ) ;
#33354=ORIENTED_EDGE ( 'NONE', *, *, #1659, .F. ) ;
#33378=FACE_OUTER_BOUND ( 'NONE', #23065, .T. ) ;
#33397=VECTOR ( 'NONE', #21963, 1000.000000000000000 ) ;
#33399=DIRECTION ( 'NONE',  ( -1.000000000000000000, 0.000000000000000000, 0.000000000000000000 ) ) ;
#33406=DIRECTION ( 'NONE',  ( 0.000000000000000000, -0.5877852522924621459, -0.8090169943749555559 ) ) ;
#33417=VECTOR ( 'NONE', #26313, 1000.000000000000000 ) ;
#33436=DIRECTION ( 'NONE',  ( -1.000000000000000000, 0.000000000000000000, 0.000000000000000000 ) ) ;
#33443=ORIENTED_EDGE ( 'NONE', *, *, #34780, .T. ) ;
#33457=CARTESIAN_POINT ( 'NONE',  ( 0.000000000000000000, 0.000000000000000000, 0.000000000000000000 ) ) ;
#33473=DIRECTION ( 'NONE',  ( 0.000000000000000000, 0.000000000000000000, 1.000000000000000000 ) ) ;
#33478=EDGE_CURVE ( 'NONE', #23042, #24581, #2371, .T. ) ;
#33497=CARTESIAN_POINT ( 'NONE',  ( 0.000000000000000000, 0.000000000000000000, 0.000000000000000000 ) ) ;
#33513=ORIENTED_EDGE ( 'NONE', *, *, #23772, .F. ) ;
#33517=AXIS2_PLACEMENT_3D ( 'NONE', #2810, #24754, #21319 ) ;
#33532=ORIENTED_EDGE ( 'NONE', *, *, #26844, .F. ) ;
#33540=DIRECTION ( 'NONE',  ( 0.000000000000000000, -0.8090169943749534465, 0.5877852522924649215 ) ) ;
#33542=CIRCLE ( 'NONE', #5947, 4.000000000000000000 ) ;
#33548=ADVANCED_FACE ( 'NONE', ( #12671 ), #5416, .T. ) ;
#33569=VECTOR ( 'NONE', #23128, 1000.000000000000000 ) ;
#33572=DIRECTION ( 'NONE',  ( -1.000000000000000000, 0.000000000000000000, 0.000000000000000000 ) ) ;
#33574=LINE ( 'NONE', #8905, #30475 ) ;
#33576=CARTESIAN_POINT ( 'NONE',  ( 0.000000000000000000, -21.80633394113448276, -2.912696353506054159 ) ) ;
#33577=DIRECTION ( 'NONE',  ( -1.000000000000000000, 0.000000000000000000, 0.000000000000000000 ) ) ;
#33590=ORIENTED_EDGE ( 'NONE', *, *, #17935, .F. ) ;
#33600=ORIENTED_EDGE ( 'NONE', *, *, #6603, .F. ) ;
#33605=CARTESIAN_POINT ( 'NONE',  ( 8.000000000000000000, -16.53603053422202862, -8.931325931664767737 ) ) ;
#33606=PRODUCT_CONTEXT ( 'NONE', #1346, 'mechanical' ) ;
#33621=CARTESIAN_POINT ( 'NONE',  ( 0.000000000000000000, -3.384281271887945586, 18.48663108841355651 ) ) ;
#33624=DIRECTION ( 'NONE',  ( 0.000000000000000000, -0.5877852522924799095, 0.8090169943749424553 ) ) ;
#33630=ORIENTED_EDGE ( 'NONE', *, *, #25959, .T. ) ;
#33654=ORIENTED_EDGE ( 'NONE', *, *, #1547, .T. ) ;
#33669=CARTESIAN_POINT ( 'NONE',  ( 0.000000000000000000, 5.400000000000013678, 5.082197683525802034E-18 ) ) ;
#33671=CARTESIAN_POINT ( 'NONE',  ( 8.000000000000000000, 9.508666619816938947, -19.83898331853677277 ) ) ;
#33693=CIRCLE ( 'NONE', #30818, 8.000000000000008882 ) ;
#33714=CARTESIAN_POINT ( 'NONE',  ( 50.00005079999999680, 5.399999999999999467, -1.000000000000003109 ) ) ;
#33728=CIRCLE ( 'NONE', #6713, 4.000000000000000000 ) ;
#33781=AXIS2_PLACEMENT_3D ( 'NONE', #10217, #4117, #17941 ) ;
#33787=CYLINDRICAL_SURFACE ( 'NONE', #16981, 8.000000000000001776 ) ;
#33797=ORIENTED_EDGE ( 'NONE', *, *, #4954, .T. ) ;
#33802=CYLINDRICAL_SURFACE ( 'NONE', #99, 22.00000000000000000 ) ;
#33816=DIRECTION ( 'NONE',  ( 0.000000000000000000, -0.5877852522924796874, 0.8090169943749426773 ) ) ;
#33835=AXIS2_PLACEMENT_3D ( 'NONE', #13606, #19006, #16285 ) ;
#33837=AXIS2_PLACEMENT_3D ( 'NONE', #12729, #32657, #27443 ) ;
#33839=EDGE_LOOP ( 'NONE', ( #32052, #22380, #7462, #3708 ) ) ;
#33855=EDGE_CURVE ( 'NONE', #869, #15169, #25790, .T. ) ;
#33882=EDGE_LOOP ( 'NONE', ( #12050, #8086, #34068, #3456 ) ) ;
#33885=VERTEX_POINT ( 'NONE', #23197 ) ;
#33891=EDGE_CURVE ( 'NONE', #23346, #19686, #1961, .T. ) ;
#33930=ORIENTED_EDGE ( 'NONE', *, *, #450, .F. ) ;
#33939=DIRECTION ( 'NONE',  ( -1.000000000000000000, 0.000000000000000000, 0.000000000000000000 ) ) ;
#33944=CARTESIAN_POINT ( 'NONE',  ( 8.000000000000000000, 18.48663108841359559, -3.384281271887881637 ) ) ;
#33953=CARTESIAN_POINT ( 'NONE',  ( 8.000000000000000000, 0.000000000000000000, 0.000000000000000000 ) ) ;
#33978=AXIS2_PLACEMENT_3D ( 'NONE', #24685, #30087, #32782 ) ;
#33989=CARTESIAN_POINT ( 'NONE',  ( 8.000000000000000000, 19.35373470438997856, -10.46102064772319729 ) ) ;
#33999=MECHANICAL_DESIGN_GEOMETRIC_PRESENTATION_REPRESENTATION('',(#20759),#25391);
#34010=DIRECTION ( 'NONE',  ( -1.000000000000000000, 0.000000000000000000, 0.000000000000000000 ) ) ;
#34030=LINE ( 'NONE', #6650, #17789 ) ;
#34041=CARTESIAN_POINT ( 'NONE',  ( 0.000000000000000000, 0.000000000000000000, 0.000000000000000000 ) ) ;
#34068=ORIENTED_EDGE ( 'NONE', *, *, #9733, .T. ) ;
#34073=AXIS2_PLACEMENT_3D ( 'NONE', #29256, #4601, #29430 ) ;
#34081=UNCERTAINTY_MEASURE_WITH_UNIT (LENGTH_MEASURE( 1.000000000000000082E-05 ), #32650, 'distance_accuracy_value', 'NONE');
#34093=EDGE_CURVE ( 'NONE', #5736, #12434, #24077, .T. ) ;
#34100=VERTEX_POINT ( 'NONE', #33086 ) ;
#34101=CARTESIAN_POINT ( 'NONE',  ( 8.000000000000000000, 6.336799421340039373, -16.31134495048478428 ) ) ;
#34122=EDGE_CURVE ( 'NONE', #28798, #4346, #17382, .T. ) ;
#34129=DIRECTION ( 'NONE',  ( 0.000000000000000000, -1.000000000000000000, -1.047252562447196865E-14 ) ) ;
#34133=CARTESIAN_POINT ( 'NONE',  ( 0.000000000000000000, -19.35373470438990395, 10.46102064772334295 ) ) ;
#34136=DIRECTION ( 'NONE',  ( 0.000000000000000000, 0.000000000000000000, 1.000000000000000000 ) ) ;
#34144=ORIENTED_EDGE ( 'NONE', *, *, #6134, .T. ) ;
#34146=VECTOR ( 'NONE', #20156, 1000.000000000000000 ) ;
#34155=DIRECTION ( 'NONE',  ( -1.000000000000000000, 0.000000000000000000, 0.000000000000000000 ) ) ;
#34160=ORIENTED_EDGE ( 'NONE', *, *, #12316, .T. ) ;
#34183=VERTEX_POINT ( 'NONE', #6243 ) ;
#34192=ORIENTED_EDGE ( 'NONE', *, *, #32103, .T. ) ;
#34215=DIRECTION ( 'NONE',  ( -1.000000000000000000, 0.000000000000000000, 0.000000000000000000 ) ) ;
#34227=ORIENTED_EDGE ( 'NONE', *, *, #23845, .T. ) ;
#34232=CARTESIAN_POINT ( 'NONE',  ( 4.000000000000003553, 21.80633394113452539, 2.912696353505896063 ) ) ;
#34251=VERTEX_POINT ( 'NONE', #26045 ) ;
#34253=AXIS2_PLACEMENT_3D ( 'NONE', #5327, #16269, #5677 ) ;
#34256=LINE ( 'NONE', #9589, #20829 ) ;
#34276=CIRCLE ( 'NONE', #6658, 17.49900000000000233 ) ;
#34285=ORIENTED_EDGE ( 'NONE', *, *, #24604, .F. ) ;
#34315=DIRECTION ( 'NONE',  ( 0.000000000000000000, 0.000000000000000000, 1.000000000000000000 ) ) ;
#34321=CYLINDRICAL_SURFACE ( 'NONE', #315, 17.49900000000000233 ) ;
#34328=ORIENTED_EDGE ( 'NONE', *, *, #7385, .T. ) ;
#34340=ORIENTED_EDGE ( 'NONE', *, *, #32436, .F. ) ;
#34342=EDGE_CURVE ( 'NONE', #31433, #35453, #2749, .T. ) ;
#34348=CYLINDRICAL_SURFACE ( 'NONE', #7314, 8.000000000000001776 ) ;
#34353=CARTESIAN_POINT ( 'NONE',  ( 50.00005079999999680, 0.000000000000000000, 0.000000000000000000 ) ) ;
#34360=EDGE_CURVE ( 'NONE', #27914, #6627, #21104, .T. ) ;
#34366=CARTESIAN_POINT ( 'NONE',  ( 8.000000000000000000, 0.000000000000000000, 0.000000000000000000 ) ) ;
#34379=EDGE_CURVE ( 'NONE', #17966, #16592, #29178, .T. ) ;
#34381=AXIS2_PLACEMENT_3D ( 'NONE', #16390, #34215, #3985 ) ;
#34385=EDGE_CURVE ( 'NONE', #2111, #25342, #35053, .T. ) ;
#34394=EDGE_CURVE ( 'NONE', #7117, #1847, #31994, .T. ) ;
#34410=CARTESIAN_POINT ( 'NONE',  ( 8.000000000000000000, -21.80633394113447920, -2.912696353506051494 ) ) ;
#34415=AXIS2_PLACEMENT_3D ( 'NONE', #4105, #34155, #32163 ) ;
#34416=LINE ( 'NONE', #9732, #34146 ) ;
#34417=EDGE_LOOP ( 'NONE', ( #6062, #22374, #34192, #6191 ) ) ;
#34427=EDGE_CURVE ( 'NONE', #16647, #29296, #11861, .T. ) ;
#34434=CARTESIAN_POINT ( 'NONE',  ( 0.000000000000000000, 9.471478019455348729, -14.71414642875945056 ) ) ;
#34436=VERTEX_POINT ( 'NONE', #32692 ) ;
#34442=CARTESIAN_POINT ( 'NONE',  ( 0.000000000000000000, 19.35373470438998211, -10.46102064772319729 ) ) ;
#34445=EDGE_CURVE ( 'NONE', #5380, #6627, #19166, .T. ) ;
#34449=CYLINDRICAL_SURFACE ( 'NONE', #7047, 17.49900000000000233 ) ;
#34474=( LENGTH_UNIT ( ) NAMED_UNIT ( * ) SI_UNIT ( .MILLI., .METRE. ) );
#34482=DIRECTION ( 'NONE',  ( -1.000000000000000000, 0.000000000000000000, 0.000000000000000000 ) ) ;
#34494=CARTESIAN_POINT ( 'NONE',  ( 8.000000000000000000, -3.384281271887945586, 18.48663108841355651 ) ) ;
#34510=VERTEX_POINT ( 'NONE', #30865 ) ;
#34512=VERTEX_POINT ( 'NONE', #17336 ) ;
#34513=AXIS2_PLACEMENT_3D ( 'NONE', #8031, #5349, #19014 ) ;
#34530=VECTOR ( 'NONE', #7989, 1000.000000000000000 ) ;
#34534=CARTESIAN_POINT ( 'NONE',  ( 0.000000000000000000, 0.000000000000000000, 0.000000000000000000 ) ) ;
#34538=DIRECTION ( 'NONE',  ( -1.000000000000000000, 0.000000000000000000, 0.000000000000000000 ) ) ;
#34549=EDGE_CURVE ( 'NONE', #22962, #27214, #5682, .T. ) ;
#34550=PRODUCT ( 'spur gear_iso_ISO - Spur gear 2M 20T 20PA 8FW ---S20A75H50L8.0S1', 'spur gear_iso_ISO - Spur gear 2M 20T 20PA 8FW ---S20A75H50L8.0S1', '', ( #33606 ) ) ;
#34570=VECTOR ( 'NONE', #19258, 1000.000000000000000 ) ;
#34573=LINE ( 'NONE', #9888, #10819 ) ;
#34580=DIRECTION ( 'NONE',  ( 0.000000000000000000, 0.000000000000000000, 1.000000000000000000 ) ) ;
#34589=ORIENTED_EDGE ( 'NONE', *, *, #8721, .T. ) ;
#34594=LINE ( 'NONE', #34232, #33417 ) ;
#34598=VECTOR ( 'NONE', #12202, 1000.000000000000000 ) ;
#34606=LINE ( 'NONE', #11918, #18829 ) ;
#34625=EDGE_CURVE ( 'NONE', #34512, #7954, #24525, .T. ) ;
#34629=DIRECTION ( 'NONE',  ( 0.000000000000000000, 0.000000000000000000, 1.000000000000000000 ) ) ;
#34650=( NAMED_UNIT ( * ) SI_UNIT ( $, .STERADIAN. ) SOLID_ANGLE_UNIT ( ) );
#34669=CARTESIAN_POINT ( 'NONE',  ( 8.000000000000000000, -14.71414642875963708, 9.471478019455089381 ) ) ;
#34672=FACE_OUTER_BOUND ( 'NONE', #26499, .T. ) ;
#34681=CARTESIAN_POINT ( 'NONE',  ( 0.000000000000000000, 0.000000000000000000, 0.000000000000000000 ) ) ;
#34692=VERTEX_POINT ( 'NONE', #34101 ) ;
#34704=AXIS2_PLACEMENT_3D ( 'NONE', #319, #11311, #33276 ) ;
#34712=CARTESIAN_POINT ( 'NONE',  ( 0.000000000000000000, -16.31134495048480559, -6.336799421339987859 ) ) ;
#34716=AXIS2_PLACEMENT_3D ( 'NONE', #2, #5069, #29724 ) ;
#34729=VERTEX_POINT ( 'NONE', #3870 ) ;
#34739=VERTEX_POINT ( 'NONE', #23100 ) ;
#34743=CARTESIAN_POINT ( 'NONE',  ( 8.000000000000000000, 9.508666619816654730, 19.83898331853691488 ) ) ;
#34752=DIRECTION ( 'NONE',  ( -1.000000000000000000, 0.000000000000000000, 0.000000000000000000 ) ) ;
#34759=CARTESIAN_POINT ( 'NONE',  ( 0.000000000000000000, -12.96676809804157848, 13.60411018104313641 ) ) ;
#34780=EDGE_CURVE ( 'NONE', #26182, #15733, #31424, .T. ) ;
#34803=ORIENTED_EDGE ( 'NONE', *, *, #29066, .F. ) ;
#34814=CARTESIAN_POINT ( 'NONE',  ( 0.000000000000000000, 4.460989585141205360, -16.92083251265322730 ) ) ;
#34817=CIRCLE ( 'NONE', #25019, 22.00000000000000000 ) ;
#34821=DIRECTION ( 'NONE',  ( 0.000000000000000000, 0.000000000000000000, 1.000000000000000000 ) ) ;
#34850=CARTESIAN_POINT ( 'NONE',  ( 0.000000000000000000, 0.000000000000000000, 0.000000000000000000 ) ) ;
#34860=ORIENTED_EDGE ( 'NONE', *, *, #4540, .T. ) ;
#34881=CIRCLE ( 'NONE', #24542, 8.000000000000000000 ) ;
#34894=CYLINDRICAL_SURFACE ( 'NONE', #33781, 17.49900000000000233 ) ;
#34901=FACE_OUTER_BOUND ( 'NONE', #6981, .T. ) ;
#34903=CARTESIAN_POINT ( 'NONE',  ( 8.000000000000000000, 16.92083251265334098, -4.460989585140788805 ) ) ;
#34914=ORIENTED_EDGE ( 'NONE', *, *, #5262, .F. ) ;
#34932=CIRCLE ( 'NONE', #6738, 22.00000000000000000 ) ;
#34941=CIRCLE ( 'NONE', #3887, 8.000000000000007105 ) ;
#34947=CYLINDRICAL_SURFACE ( 'NONE', #27418, 8.000000000000003553 ) ;
#34952=CARTESIAN_POINT ( 'NONE',  ( 0.000000000000000000, -13.55483219355736324, 11.06713717293235710 ) ) ;
#34963=DIRECTION ( 'NONE',  ( -1.000000000000000000, 0.000000000000000000, 0.000000000000000000 ) ) ;
#34975=FACE_OUTER_BOUND ( 'NONE', #24488, .T. ) ;
#34980=DIRECTION ( 'NONE',  ( 0.000000000000000000, 0.000000000000000000, -1.000000000000000000 ) ) ;
#35010=VERTEX_POINT ( 'NONE', #22700 ) ;
#35011=ORIENTED_EDGE ( 'NONE', *, *, #5919, .F. ) ;
#35015=EDGE_CURVE ( 'NONE', #9304, #22471, #32997, .T. ) ;
#35017=FILL_AREA_STYLE_COLOUR ( '', #2966 ) ;
#35033=CARTESIAN_POINT ( 'NONE',  ( 0.000000000000000000, -8.931325931664709117, 16.53603053422203573 ) ) ;
#35035=AXIS2_PLACEMENT_3D ( 'NONE', #2468, #24080, #29831 ) ;
#35044=DIRECTION ( 'NONE',  ( -1.000000000000000000, 0.000000000000000000, 0.000000000000000000 ) ) ;
#35053=LINE ( 'NONE', #10543, #21023 ) ;
#35066=EDGE_CURVE ( 'NONE', #25795, #3084, #29008, .T. ) ;
#35069=ORIENTED_EDGE ( 'NONE', *, *, #12507, .F. ) ;
#35071=FACE_OUTER_BOUND ( 'NONE', #13204, .T. ) ;
#35077=DIRECTION ( 'NONE',  ( 0.000000000000000000, 0.5877852522924682521, 0.8090169943749511150 ) ) ;
#35107=EDGE_LOOP ( 'NONE', ( #35477, #33513, #17110, #12909 ) ) ;
#35114=DIRECTION ( 'NONE',  ( -1.000000000000000000, 0.000000000000000000, 0.000000000000000000 ) ) ;
#35152=ORIENTED_EDGE ( 'NONE', *, *, #18986, .F. ) ;
#35187=CIRCLE ( 'NONE', #28845, 8.000000000000001776 ) ;
#35199=CARTESIAN_POINT ( 'NONE',  ( 0.000000000000000000, 8.931325931664870765, -16.53603053422199665 ) ) ;
#35216=DIRECTION ( 'NONE',  ( 0.000000000000000000, 0.000000000000000000, 1.000000000000000000 ) ) ;
#35223=ORIENTED_EDGE ( 'NONE', *, *, #12263, .F. ) ;
#35225=DIRECTION ( 'NONE',  ( -1.000000000000000000, 0.000000000000000000, 0.000000000000000000 ) ) ;
#35226=CARTESIAN_POINT ( 'NONE',  ( 8.000000000000000000, 0.000000000000000000, 0.000000000000000000 ) ) ;
#35232=ORIENTED_EDGE ( 'NONE', *, *, #30371, .F. ) ;
#35233=ORIENTED_EDGE ( 'NONE', *, *, #34342, .F. ) ;
#35253=VECTOR ( 'NONE', #30712, 1000.000000000000000 ) ;
#35261=FACE_OUTER_BOUND ( 'NONE', #11390, .T. ) ;
#35273=ORIENTED_EDGE ( 'NONE', *, *, #34385, .F. ) ;
#35292=CIRCLE ( 'NONE', #3648, 22.00000000000000000 ) ;
#35314=DIRECTION ( 'NONE',  ( -1.000000000000000000, 0.000000000000000000, 0.000000000000000000 ) ) ;
#35339=DIRECTION ( 'NONE',  ( 0.000000000000000000, 0.000000000000000000, 1.000000000000000000 ) ) ;
#35343=CYLINDRICAL_SURFACE ( 'NONE', #7918, 8.000000000000001776 ) ;
#35359=CARTESIAN_POINT ( 'NONE',  ( 0.000000000000000000, 0.000000000000000000, 0.000000000000000000 ) ) ;
#35374=AXIS2_PLACEMENT_3D ( 'NONE', #14233, #22159, #13725 ) ;
#35383=ORIENTED_EDGE ( 'NONE', *, *, #33233, .T. ) ;
#35385=DIRECTION ( 'NONE',  ( -1.000000000000000000, 0.000000000000000000, 0.000000000000000000 ) ) ;
#35387=AXIS2_PLACEMENT_3D ( 'NONE', #19705, #22594, #14147 ) ;
#35391=DIRECTION ( 'NONE',  ( 0.000000000000000000, 0.000000000000000000, -1.000000000000000000 ) ) ;
#35394=ORIENTED_EDGE ( 'NONE', *, *, #2711, .T. ) ;
#35402=CIRCLE ( 'NONE', #26188, 8.000000000000000000 ) ;
#35411=AXIS2_PLACEMENT_3D ( 'NONE', #10363, #21323, #5152 ) ;
#35416=CIRCLE ( 'NONE', #29083, 8.000000000000007105 ) ;
#35419=DIRECTION ( 'NONE',  ( 1.000000000000000000, -0.000000000000000000, -0.000000000000000000 ) ) ;
#35426=CARTESIAN_POINT ( 'NONE',  ( 8.000000000000000000, -8.128228055638974325, 16.94522934049209795 ) ) ;
#35427=SURFACE_STYLE_FILL_AREA ( #13810 ) ;
#35434=ORIENTED_EDGE ( 'NONE', *, *, #18796, .F. ) ;
#35453=VERTEX_POINT ( 'NONE', #14210 ) ;
#35465=CARTESIAN_POINT ( 'NONE',  ( 8.000000000000000000, -16.92083251265322374, -4.460989585141144076 ) ) ;
#35471=CIRCLE ( 'NONE', #7283, 8.000000000000007105 ) ;
#35477=ORIENTED_EDGE ( 'NONE', *, *, #664, .T. ) ;
#35487=ADVANCED_FACE ( 'NONE', ( #27736 ), #13698, .T. ) ;
#35519=CARTESIAN_POINT ( 'NONE',  ( 8.000000000000000000, -18.48663108841356717, 4.615718728111985136 ) ) ;
#35526=CIRCLE ( 'NONE', #7898, 8.000000000000008882 ) ;
#35532=ADVANCED_FACE ( 'NONE', ( #22484 ), #27902, .T. ) ;
#35536=CARTESIAN_POINT ( 'NONE',  ( 8.000000000000000000, -15.92965478239629817, 15.17386234660377831 ) ) ;
#35553=DIRECTION ( 'NONE',  ( 0.000000000000000000, 0.000000000000000000, 1.000000000000000000 ) ) ;
#35555=LINE ( 'NONE', #27089, #27754 ) ;
#35565=ORIENTED_EDGE ( 'NONE', *, *, #10018, .T. ) ;
#35573=LINE ( 'NONE', #13417, #1541 ) ;
#35577=DIRECTION ( 'NONE',  ( 0.000000000000000000, 0.000000000000000000, 1.000000000000000000 ) ) ;
#35579=FACE_OUTER_BOUND ( 'NONE', #18421, .T. ) ;
#35580=CARTESIAN_POINT ( 'NONE',  ( 8.000000000000000000, -14.71414642875963708, 9.471478019455089381 ) ) ;
#35592=DIRECTION ( 'NONE',  ( -1.000000000000000000, 0.000000000000000000, 0.000000000000000000 ) ) ;
#35598=CARTESIAN_POINT ( 'NONE',  ( 8.000000000000000000, 0.000000000000000000, 0.000000000000000000 ) ) ;
#35610=ORIENTED_EDGE ( 'NONE', *, *, #4150, .T. ) ;
ENDSEC;
END-ISO-10303-21;
